ISO-10303-21;
HEADER;
FILE_DESCRIPTION (('STEP AP214'),
    '1' );
FILE_NAME ('Servo-Body.step',
    '2026-11-01T05:08:46',
    ( '' ),
    ( '' ),
    'SwSTEP 2.0',
    'SolidWorks 2024',
    '' );
FILE_SCHEMA (( 'AUTOMOTIVE_DESIGN' ));
ENDSEC;

DATA;
#4=PLANE ( 'NONE',  #1981 ) ;
#13=AXIS2_PLACEMENT_3D ( 'NONE', #1699, #13214, #4196 ) ;
#15=VERTEX_POINT ( 'NONE', #6496 ) ;
#17=CYLINDRICAL_SURFACE ( 'NONE', #5319, 8.000000000000000000 ) ;
#23=VECTOR ( 'NONE', #3492, 1000.000000000000000 ) ;
#32=ORIENTED_EDGE ( 'NONE', *, *, #4689, .T. ) ;
#44=FILL_AREA_STYLE_COLOUR ( '', #16509 ) ;
#69=EDGE_CURVE ( 'NONE', #1150, #1326, #513, .T. ) ;
#73=DIRECTION ( 'NONE',  ( 0.000000000000000000, 0.000000000000000000, -1.000000000000000000 ) ) ;
#82=ORIENTED_EDGE ( 'NONE', *, *, #2919, .T. ) ;
#96=DIRECTION ( 'NONE',  ( -1.000000000000000000, -0.000000000000000000, -0.000000000000000000 ) ) ;
#148=DIRECTION ( 'NONE',  ( -0.000000000000000000, -1.000000000000000000, 0.000000000000000000 ) ) ;
#170=EDGE_CURVE ( 'NONE', #13772, #6368, #9349, .T. ) ;
#172=CARTESIAN_POINT ( 'NONE',  ( -22.99999999999999645, 0.000000000000000000, 37.00000000000002132 ) ) ;
#189=EDGE_CURVE ( 'NONE', #1698, #9930, #6838, .T. ) ;
#191=CARTESIAN_POINT ( 'NONE',  ( 31.00000000000002842, 68.00000000000000000, 26.00000000000001066 ) ) ;
#215=DIRECTION ( 'NONE',  ( 0.000000000000000000, 0.000000000000000000, -1.000000000000000000 ) ) ;
#229=DIRECTION ( 'NONE',  ( 1.000000000000000000, 0.000000000000000000, -0.000000000000000000 ) ) ;
#275=DIRECTION ( 'NONE',  ( -0.000000000000000000, -1.000000000000000000, -0.000000000000000000 ) ) ;
#299=DIRECTION ( 'NONE',  ( 0.000000000000000000, 0.000000000000000000, -1.000000000000000000 ) ) ;
#304=PLANE ( 'NONE',  #11954 ) ;
#315=CARTESIAN_POINT ( 'NONE',  ( 30.99999999999999645, 68.00000000000000000, 31.00000000000001066 ) ) ;
#346=AXIS2_PLACEMENT_3D ( 'NONE', #5063, #9108, #2577 ) ;
#373=EDGE_CURVE ( 'NONE', #3758, #6942, #6476, .T. ) ;
#387=EDGE_CURVE ( 'NONE', #4246, #5336, #14308, .T. ) ;
#400=FACE_BOUND ( 'NONE', #5435, .T. ) ;
#412=DIRECTION ( 'NONE',  ( 0.000000000000000000, 0.000000000000000000, -1.000000000000000000 ) ) ;
#420=ORIENTED_EDGE ( 'NONE', *, *, #5520, .F. ) ;
#438=ORIENTED_EDGE ( 'NONE', *, *, #9102, .F. ) ;
#457=ORIENTED_EDGE ( 'NONE', *, *, #6897, .F. ) ;
#467=ORIENTED_EDGE ( 'NONE', *, *, #1204, .F. ) ;
#481=DIRECTION ( 'NONE',  ( 0.000000000000000000, 0.000000000000000000, 1.000000000000000000 ) ) ;
#500=CYLINDRICAL_SURFACE ( 'NONE', #1121, 7.999999999999996447 ) ;
#513=LINE ( 'NONE', #16050, #5810 ) ;
#528=LINE ( 'NONE', #10654, #16885 ) ;
#540=EDGE_CURVE ( 'NONE', #4246, #12484, #6999, .T. ) ;
#612=AXIS2_PLACEMENT_3D ( 'NONE', #4088, #1336, #229 ) ;
#634=ORIENTED_EDGE ( 'NONE', *, *, #1223, .F. ) ;
#640=DIRECTION ( 'NONE',  ( -0.000000000000000000, -1.000000000000000000, 0.000000000000000000 ) ) ;
#658=VECTOR ( 'NONE', #11518, 1000.000000000000000 ) ;
#666=FACE_OUTER_BOUND ( 'NONE', #12649, .T. ) ;
#671=ADVANCED_FACE ( 'NONE', ( #4669 ), #16283, .F. ) ;
#705=ORIENTED_EDGE ( 'NONE', *, *, #11811, .T. ) ;
#719=DIRECTION ( 'NONE',  ( -1.000000000000000000, -0.000000000000000000, -0.000000000000000000 ) ) ;
#735=CYLINDRICAL_SURFACE ( 'NONE', #9556, 4.999999999999997335 ) ;
#737=PLANE ( 'NONE',  #10255 ) ;
#809=EDGE_CURVE ( 'NONE', #6970, #15231, #5008, .T. ) ;
#823=DIRECTION ( 'NONE',  ( 1.000000000000000000, -0.000000000000000000, 0.000000000000000000 ) ) ;
#841=AXIS2_PLACEMENT_3D ( 'NONE', #16046, #1536, #10634 ) ;
#857=DIRECTION ( 'NONE',  ( 0.000000000000000000, 0.000000000000000000, -1.000000000000000000 ) ) ;
#868=PLANE ( 'NONE',  #5746 ) ;
#894=FACE_OUTER_BOUND ( 'NONE', #3103, .T. ) ;
#902=AXIS2_PLACEMENT_3D ( 'NONE', #9006, #9176, #73 ) ;
#931=ORIENTED_EDGE ( 'NONE', *, *, #10790, .F. ) ;
#938=ORIENTED_EDGE ( 'NONE', *, *, #13325, .F. ) ;
#946=DIRECTION ( 'NONE',  ( -0.000000000000000000, -1.000000000000000000, -0.000000000000000000 ) ) ;
#956=VECTOR ( 'NONE', #13594, 1000.000000000000000 ) ;
#962=ADVANCED_FACE ( 'NONE', ( #9310 ), #15745, .F. ) ;
#983=LINE ( 'NONE', #12831, #15918 ) ;
#992=ADVANCED_FACE ( 'NONE', ( #10764 ), #3994, .T. ) ;
#1040=EDGE_LOOP ( 'NONE', ( #5659, #15885, #8082, #11990 ) ) ;
#1054=EDGE_LOOP ( 'NONE', ( #15987, #9860, #7839, #7816 ) ) ;
#1085=CARTESIAN_POINT ( 'NONE',  ( 23.00000000000000711, 68.00000000000000000, -36.99999999999999289 ) ) ;
#1094=VECTOR ( 'NONE', #412, 1000.000000000000000 ) ;
#1119=DIRECTION ( 'NONE',  ( 0.000000000000000000, -0.000000000000000000, -1.000000000000000000 ) ) ;
#1121=AXIS2_PLACEMENT_3D ( 'NONE', #5551, #10800, #4365 ) ;
#1130=FACE_OUTER_BOUND ( 'NONE', #6538, .T. ) ;
#1150=VERTEX_POINT ( 'NONE', #4110 ) ;
#1152=DIRECTION ( 'NONE',  ( 0.000000000000000000, 0.000000000000000000, -1.000000000000000000 ) ) ;
#1180=CARTESIAN_POINT ( 'NONE',  ( 23.00000000000000711, 68.00000000000000000, -31.00000000000002487 ) ) ;
#1181=DIRECTION ( 'NONE',  ( 0.000000000000000000, 0.000000000000000000, -1.000000000000000000 ) ) ;
#1204=EDGE_CURVE ( 'NONE', #6942, #10732, #11840, .T. ) ;
#1223=EDGE_CURVE ( 'NONE', #16701, #16577, #11838, .T. ) ;
#1237=DIRECTION ( 'NONE',  ( 1.000000000000000000, 0.000000000000000000, 0.000000000000000000 ) ) ;
#1242=LINE ( 'NONE', #5255, #7128 ) ;
#1252=DIRECTION ( 'NONE',  ( -0.000000000000000000, -0.000000000000000000, 1.000000000000000000 ) ) ;
#1264=CARTESIAN_POINT ( 'NONE',  ( 40.00000000000000000, 68.00000000000000000, 26.00000000000000355 ) ) ;
#1293=LINE ( 'NONE', #11850, #3847 ) ;
#1300=ORIENTED_EDGE ( 'NONE', *, *, #809, .F. ) ;
#1302=DIRECTION ( 'NONE',  ( 1.000000000000000000, 0.000000000000000000, 0.000000000000000000 ) ) ;
#1325=FACE_OUTER_BOUND ( 'NONE', #3982, .T. ) ;
#1326=VERTEX_POINT ( 'NONE', #10906 ) ;
#1336=DIRECTION ( 'NONE',  ( 0.000000000000000000, 0.000000000000000000, 1.000000000000000000 ) ) ;
#1353=LINE ( 'NONE', #6922, #15709 ) ;
#1376=DIRECTION ( 'NONE',  ( 1.000000000000000000, 0.000000000000000000, -1.156482317317883755E-15 ) ) ;
#1388=ADVANCED_FACE ( 'NONE', ( #10815 ), #13110, .T. ) ;
#1412=( LENGTH_UNIT ( ) NAMED_UNIT ( * ) SI_UNIT ( .MILLI., .METRE. ) );
#1416=VECTOR ( 'NONE', #9299, 1000.000000000000000 ) ;
#1417=EDGE_CURVE ( 'NONE', #12484, #1150, #2881, .T. ) ;
#1439=EDGE_CURVE ( 'NONE', #6319, #15231, #6639, .T. ) ;
#1453=DIRECTION ( 'NONE',  ( 0.000000000000000000, 0.000000000000000000, -1.000000000000000000 ) ) ;
#1487=VECTOR ( 'NONE', #16481, 1000.000000000000000 ) ;
#1488=AXIS2_PLACEMENT_3D ( 'NONE', #3280, #8693, #15217 ) ;
#1514=CARTESIAN_POINT ( 'NONE',  ( 31.00000000000002842, 68.00000000000000000, 23.00000000000001066 ) ) ;
#1516=DIRECTION ( 'NONE',  ( 0.000000000000000000, 0.000000000000000000, -1.000000000000000000 ) ) ;
#1531=AXIS2_PLACEMENT_3D ( 'NONE', #5439, #8110, #13182 ) ;
#1534=ORIENTED_EDGE ( 'NONE', *, *, #6080, .F. ) ;
#1536=DIRECTION ( 'NONE',  ( 0.000000000000000000, 0.000000000000000000, 1.000000000000000000 ) ) ;
#1548=VECTOR ( 'NONE', #1697, 1000.000000000000000 ) ;
#1556=ORIENTED_EDGE ( 'NONE', *, *, #12023, .T. ) ;
#1595=CARTESIAN_POINT ( 'NONE',  ( -22.99999999999999645, 0.000000000000000000, 37.00000000000002132 ) ) ;
#1645=VECTOR ( 'NONE', #16850, 1000.000000000000000 ) ;
#1649=ORIENTED_EDGE ( 'NONE', *, *, #7457, .T. ) ;
#1674=CARTESIAN_POINT ( 'NONE',  ( 37.00000000000000000, 68.00000000000000000, 23.00000000000001066 ) ) ;
#1675=LINE ( 'NONE', #14653, #3677 ) ;
#1697=DIRECTION ( 'NONE',  ( -0.000000000000000000, -1.000000000000000000, -0.000000000000000000 ) ) ;
#1698=VERTEX_POINT ( 'NONE', #13953 ) ;
#1699=CARTESIAN_POINT ( 'NONE',  ( -40.00000000000000000, 68.00000000000000000, -25.99999999999999645 ) ) ;
#1711=DIRECTION ( 'NONE',  ( -0.000000000000000000, -1.000000000000000000, 0.000000000000000000 ) ) ;
#1714=ORIENTED_EDGE ( 'NONE', *, *, #15609, .T. ) ;
#1724=CARTESIAN_POINT ( 'NONE',  ( 26.00000000000000711, 0.000000000000000000, -31.00000000000002487 ) ) ;
#1728=ADVANCED_FACE ( 'NONE', ( #894 ), #735, .F. ) ;
#1729=EDGE_LOOP ( 'NONE', ( #2488, #15881, #3895, #9781 ) ) ;
#1747=CARTESIAN_POINT ( 'NONE',  ( -40.00000000000000000, 68.00000000000000000, 26.00000000000000355 ) ) ;
#1757=DIRECTION ( 'NONE',  ( -0.000000000000000000, -1.000000000000000000, -0.000000000000000000 ) ) ;
#1768=ORIENTED_EDGE ( 'NONE', *, *, #6702, .F. ) ;
#1785=DIRECTION ( 'NONE',  ( -0.000000000000000000, -1.000000000000000000, -0.000000000000000000 ) ) ;
#1799=FACE_OUTER_BOUND ( 'NONE', #6425, .T. ) ;
#1815=DIRECTION ( 'NONE',  ( -1.156482317317875275E-15, 0.000000000000000000, -1.000000000000000000 ) ) ;
#1836=ORIENTED_EDGE ( 'NONE', *, *, #4867, .F. ) ;
#1844=LINE ( 'NONE', #10861, #12501 ) ;
#1846=ORIENTED_EDGE ( 'NONE', *, *, #9828, .T. ) ;
#1886=DIRECTION ( 'NONE',  ( 0.000000000000000000, 0.000000000000000000, -1.000000000000000000 ) ) ;
#1891=CARTESIAN_POINT ( 'NONE',  ( 37.00000000000000000, 0.000000000000000000, -23.00000000000000000 ) ) ;
#1894=ORIENTED_EDGE ( 'NONE', *, *, #14775, .F. ) ;
#1907=ORIENTED_EDGE ( 'NONE', *, *, #12877, .F. ) ;
#1908=LINE ( 'NONE', #9991, #10254 ) ;
#1935=CARTESIAN_POINT ( 'NONE',  ( -40.00000000000000000, 68.00000000000000000, -25.99999999999999645 ) ) ;
#1952=CARTESIAN_POINT ( 'NONE',  ( 22.99999999999999645, 68.00000000000000000, 31.00000000000006750 ) ) ;
#1981=AXIS2_PLACEMENT_3D ( 'NONE', #2659, #2321, #1119 ) ;
#2001=ORIENTED_EDGE ( 'NONE', *, *, #14775, .T. ) ;
#2042=CARTESIAN_POINT ( 'NONE',  ( -30.99999999999999289, 0.000000000000000000, 31.00000000000000000 ) ) ;
#2073=DIRECTION ( 'NONE',  ( 0.000000000000000000, 0.000000000000000000, -1.000000000000000000 ) ) ;
#2077=LINE ( 'NONE', #12476, #5855 ) ;
#2078=LINE ( 'NONE', #7384, #10309 ) ;
#2083=VERTEX_POINT ( 'NONE', #7697 ) ;
#2084=ORIENTED_EDGE ( 'NONE', *, *, #7070, .F. ) ;
#2094=LINE ( 'NONE', #13954, #3383 ) ;
#2158=VECTOR ( 'NONE', #14746, 1000.000000000000000 ) ;
#2162=VERTEX_POINT ( 'NONE', #10130 ) ;
#2193=CARTESIAN_POINT ( 'NONE',  ( -25.99999999999999645, 68.00000000000000000, 31.00000000000003908 ) ) ;
#2215=ORIENTED_EDGE ( 'NONE', *, *, #16948, .T. ) ;
#2216=DIRECTION ( 'NONE',  ( -1.000000000000000000, 0.000000000000000000, 1.156482317317875472E-15 ) ) ;
#2224=ORIENTED_EDGE ( 'NONE', *, *, #15592, .F. ) ;
#2241=LINE ( 'NONE', #7640, #658 ) ;
#2248=ORIENTED_EDGE ( 'NONE', *, *, #11811, .F. ) ;
#2267=EDGE_CURVE ( 'NONE', #11960, #7984, #4354, .T. ) ;
#2272=ORIENTED_EDGE ( 'NONE', *, *, #1439, .T. ) ;
#2286=PLANE ( 'NONE',  #13168 ) ;
#2294=VERTEX_POINT ( 'NONE', #13459 ) ;
#2300=VECTOR ( 'NONE', #14206, 1000.000000000000000 ) ;
#2321=DIRECTION ( 'NONE',  ( 0.000000000000000000, -1.000000000000000000, 0.000000000000000000 ) ) ;
#2323=DIRECTION ( 'NONE',  ( 0.000000000000000000, 0.000000000000000000, -1.000000000000000000 ) ) ;
#2325=CARTESIAN_POINT ( 'NONE',  ( 31.00000000000006395, 68.00000000000000000, -22.99999999999999289 ) ) ;
#2336=ORIENTED_EDGE ( 'NONE', *, *, #7070, .T. ) ;
#2341=EDGE_CURVE ( 'NONE', #1150, #1698, #5719, .T. ) ;
#2402=CARTESIAN_POINT ( 'NONE',  ( 22.99999999999999289, 68.00000000000000000, 37.00000000000002132 ) ) ;
#2413=LINE ( 'NONE', #16921, #14094 ) ;
#2426=DIRECTION ( 'NONE',  ( -0.000000000000000000, -1.000000000000000000, -0.000000000000000000 ) ) ;
#2459=ADVANCED_FACE ( 'NONE', ( #16610 ), #15327, .F. ) ;
#2478=AXIS2_PLACEMENT_3D ( 'NONE', #14214, #11539, #6285 ) ;
#2488=ORIENTED_EDGE ( 'NONE', *, *, #14023, .F. ) ;
#2502=CLOSED_SHELL ( 'NONE', ( #16619, #10825, #12339, #15141, #3509, #1728, #12688, #5427, #9181, #962, #671, #14093, #2459, #4372, #6873, #6526, #12645, #5405, #2900, #992, #1388, #9202, #9818, #9654, #13487, #12666, #10827, #15913, #16741, #10107, #12050, #4042, #12928, #6762 ) ) ;
#2520=CARTESIAN_POINT ( 'NONE',  ( -40.00000000000000000, 68.00000000000000000, 26.00000000000000355 ) ) ;
#2536=CARTESIAN_POINT ( 'NONE',  ( -40.00000000000000000, 0.000000000000000000, -25.99999999999999645 ) ) ;
#2544=VECTOR ( 'NONE', #10813, 1000.000000000000000 ) ;
#2548=EDGE_CURVE ( 'NONE', #10447, #4210, #16858, .T. ) ;
#2550=CARTESIAN_POINT ( 'NONE',  ( -25.99999999999999645, 68.00000000000000000, 31.00000000000003908 ) ) ;
#2577=DIRECTION ( 'NONE',  ( -5.782411586589400040E-16, 0.000000000000000000, 1.000000000000000000 ) ) ;
#2579=CARTESIAN_POINT ( 'NONE',  ( 25.99999999999999645, 0.000000000000000000, 31.00000000000004619 ) ) ;
#2614=DIRECTION ( 'NONE',  ( -1.000000000000000000, 0.000000000000000000, -0.000000000000000000 ) ) ;
#2615=ORIENTED_EDGE ( 'NONE', *, *, #11497, .T. ) ;
#2616=FACE_OUTER_BOUND ( 'NONE', #11012, .T. ) ;
#2621=CARTESIAN_POINT ( 'NONE',  ( 25.99999999999999645, 68.00000000000000000, 31.00000000000004619 ) ) ;
#2622=CARTESIAN_POINT ( 'NONE',  ( 31.00000000000006395, 0.000000000000000000, -22.99999999999999289 ) ) ;
#2631=ORIENTED_EDGE ( 'NONE', *, *, #170, .T. ) ;
#2633=CARTESIAN_POINT ( 'NONE',  ( -31.00000000000003197, 68.00000000000000000, 26.00000000000000355 ) ) ;
#2659=CARTESIAN_POINT ( 'NONE',  ( -30.99999999999999645, 0.000000000000000000, -30.99999999999999289 ) ) ;
#2704=FILL_AREA_STYLE ('',( #44 ) ) ;
#2713=CARTESIAN_POINT ( 'NONE',  ( 40.00000000000000000, 0.000000000000000000, -25.99999999999999645 ) ) ;
#2721=CARTESIAN_POINT ( 'NONE',  ( 30.99999999999999645, 0.000000000000000000, 31.00000000000001066 ) ) ;
#2770=ORIENTED_EDGE ( 'NONE', *, *, #12877, .T. ) ;
#2791=EDGE_CURVE ( 'NONE', #3811, #10491, #1908, .T. ) ;
#2801=ORIENTED_EDGE ( 'NONE', *, *, #7754, .T. ) ;
#2810=ORIENTED_EDGE ( 'NONE', *, *, #8213, .T. ) ;
#2833=AXIS2_PLACEMENT_3D ( 'NONE', #6884, #1757, #299 ) ;
#2834=CARTESIAN_POINT ( 'NONE',  ( 31.00000000000000711, 0.000000000000000000, -30.99999999999999289 ) ) ;
#2845=ORIENTED_EDGE ( 'NONE', *, *, #14744, .F. ) ;
#2854=LINE ( 'NONE', #4065, #1416 ) ;
#2856=VECTOR ( 'NONE', #275, 1000.000000000000000 ) ;
#2870=CYLINDRICAL_SURFACE ( 'NONE', #1531, 4.999999999999997335 ) ;
#2872=ORIENTED_EDGE ( 'NONE', *, *, #15269, .F. ) ;
#2879=LINE ( 'NONE', #11898, #12990 ) ;
#2881=LINE ( 'NONE', #16952, #9110 ) ;
#2891=VERTEX_POINT ( 'NONE', #16500 ) ;
#2900=ADVANCED_FACE ( 'NONE', ( #1130 ), #9117, .T. ) ;
#2919=EDGE_CURVE ( 'NONE', #15508, #6970, #2241, .T. ) ;
#2953=ORIENTED_EDGE ( 'NONE', *, *, #13325, .T. ) ;
#2960=CARTESIAN_POINT ( 'NONE',  ( -40.00000000000000000, 68.00000000000000000, 26.00000000000000355 ) ) ;
#2987=DIRECTION ( 'NONE',  ( -0.000000000000000000, -1.000000000000000000, -0.000000000000000000 ) ) ;
#3012=EDGE_CURVE ( 'NONE', #4223, #15448, #7982, .T. ) ;
#3050=EDGE_CURVE ( 'NONE', #2162, #2891, #5314, .T. ) ;
#3052=DIRECTION ( 'NONE',  ( -1.000000000000000000, -0.000000000000000000, 1.156482317317883755E-15 ) ) ;
#3065=CARTESIAN_POINT ( 'NONE',  ( 26.00000000000001066, 68.00000000000000000, -31.00000000000002487 ) ) ;
#3085=DIRECTION ( 'NONE',  ( -0.000000000000000000, -1.000000000000000000, 0.000000000000000000 ) ) ;
#3103=EDGE_LOOP ( 'NONE', ( #11244, #9389, #9401, #16411 ) ) ;
#3104=CARTESIAN_POINT ( 'NONE',  ( -31.00000000000005684, 68.00000000000000000, 23.00000000000000355 ) ) ;
#3121=EDGE_CURVE ( 'NONE', #4316, #4076, #12293, .T. ) ;
#3126=CARTESIAN_POINT ( 'NONE',  ( -25.99999999999999645, 68.00000000000000000, 40.00000000000002132 ) ) ;
#3128=ORIENTED_EDGE ( 'NONE', *, *, #13080, .F. ) ;
#3144=ORIENTED_EDGE ( 'NONE', *, *, #9098, .T. ) ;
#3145=( GEOMETRIC_REPRESENTATION_CONTEXT ( 3 ) GLOBAL_UNCERTAINTY_ASSIGNED_CONTEXT ( ( #8071 ) ) GLOBAL_UNIT_ASSIGNED_CONTEXT ( ( #8513, #7210, #11252 ) ) REPRESENTATION_CONTEXT ( 'NONE', 'WORKASPACE' ) );
#3148=VECTOR ( 'NONE', #7996, 1000.000000000000000 ) ;
#3149=DIRECTION ( 'NONE',  ( -1.000000000000000000, 0.000000000000000000, 0.000000000000000000 ) ) ;
#3186=CARTESIAN_POINT ( 'NONE',  ( -22.99999999999999645, 0.000000000000000000, 31.00000000000003908 ) ) ;
#3206=CARTESIAN_POINT ( 'NONE',  ( 30.99999999999999645, 68.00000000000000000, 31.00000000000001066 ) ) ;
#3217=ORIENTED_EDGE ( 'NONE', *, *, #13080, .T. ) ;
#3222=ORIENTED_EDGE ( 'NONE', *, *, #7306, .F. ) ;
#3240=ORIENTED_EDGE ( 'NONE', *, *, #9098, .F. ) ;
#3259=CARTESIAN_POINT ( 'NONE',  ( 22.99999999999999289, 0.000000000000000000, 37.00000000000002132 ) ) ;
#3280=CARTESIAN_POINT ( 'NONE',  ( 0.000000000000000000, 0.000000000000000000, 0.000000000000000000 ) ) ;
#3284=DIRECTION ( 'NONE',  ( -0.000000000000000000, -1.000000000000000000, -0.000000000000000000 ) ) ;
#3303=DIRECTION ( 'NONE',  ( -0.000000000000000000, -1.000000000000000000, -0.000000000000000000 ) ) ;
#3312=AXIS2_PLACEMENT_3D ( 'NONE', #2520, #1152, #2614 ) ;
#3324=EDGE_CURVE ( 'NONE', #15724, #13772, #8059, .T. ) ;
#3347=CARTESIAN_POINT ( 'NONE',  ( -22.99999999999999645, 68.00000000000000000, 31.00000000000003908 ) ) ;
#3383=VECTOR ( 'NONE', #6198, 1000.000000000000000 ) ;
#3400=DIRECTION ( 'NONE',  ( -0.000000000000000000, -1.000000000000000000, -0.000000000000000000 ) ) ;
#3407=ORIENTED_EDGE ( 'NONE', *, *, #11263, .T. ) ;
#3410=CARTESIAN_POINT ( 'NONE',  ( -37.00000000000000000, 68.00000000000000000, 23.00000000000000355 ) ) ;
#3436=AXIS2_PLACEMENT_3D ( 'NONE', #12192, #4453, #15095 ) ;
#3442=VERTEX_POINT ( 'NONE', #1952 ) ;
#3491=AXIS2_PLACEMENT_3D ( 'NONE', #16750, #9032, #6427 ) ;
#3492=DIRECTION ( 'NONE',  ( -0.000000000000000000, -1.000000000000000000, -0.000000000000000000 ) ) ;
#3509=ADVANCED_FACE ( 'NONE', ( #1799 ), #9865, .F. ) ;
#3530=LINE ( 'NONE', #4479, #16841 ) ;
#3540=EDGE_CURVE ( 'NONE', #9593, #14549, #3835, .T. ) ;
#3556=CARTESIAN_POINT ( 'NONE',  ( -31.00000000000003197, 0.000000000000000000, 26.00000000000000355 ) ) ;
#3592=DIRECTION ( 'NONE',  ( -0.000000000000000000, -1.000000000000000000, -0.000000000000000000 ) ) ;
#3593=AXIS2_PLACEMENT_3D ( 'NONE', #3410, #7506, #6051 ) ;
#3596=EDGE_LOOP ( 'NONE', ( #10172, #14524, #11024, #8396 ) ) ;
#3623=CARTESIAN_POINT ( 'NONE',  ( 37.00000000000000000, 68.00000000000000000, -23.00000000000000000 ) ) ;
#3642=CIRCLE ( 'NONE', #13245, 8.000000000000000000 ) ;
#3645=CARTESIAN_POINT ( 'NONE',  ( 25.99999999999999645, 68.00000000000000000, -39.99999999999999289 ) ) ;
#3653=DIRECTION ( 'NONE',  ( -1.000000000000000000, -0.000000000000000000, -0.000000000000000000 ) ) ;
#3657=CARTESIAN_POINT ( 'NONE',  ( 23.00000000000000711, 0.000000000000000000, -36.99999999999999289 ) ) ;
#3677=VECTOR ( 'NONE', #10870, 1000.000000000000000 ) ;
#3693=ORIENTED_EDGE ( 'NONE', *, *, #12414, .F. ) ;
#3729=ORIENTED_EDGE ( 'NONE', *, *, #7179, .T. ) ;
#3758=VERTEX_POINT ( 'NONE', #2713 ) ;
#3771=LINE ( 'NONE', #9010, #16256 ) ;
#3790=CARTESIAN_POINT ( 'NONE',  ( 37.00000000000000000, 68.00000000000000000, 23.00000000000001066 ) ) ;
#3806=CARTESIAN_POINT ( 'NONE',  ( 25.99999999999999645, 68.00000000000000000, 40.00000000000002132 ) ) ;
#3811=VERTEX_POINT ( 'NONE', #13637 ) ;
#3822=ORIENTED_EDGE ( 'NONE', *, *, #9415, .F. ) ;
#3826=ORIENTED_EDGE ( 'NONE', *, *, #373, .T. ) ;
#3830=DIRECTION ( 'NONE',  ( -1.156482317317875275E-15, 0.000000000000000000, -1.000000000000000000 ) ) ;
#3835=LINE ( 'NONE', #9073, #11640 ) ;
#3838=ORIENTED_EDGE ( 'NONE', *, *, #8551, .F. ) ;
#3847=VECTOR ( 'NONE', #2323, 1000.000000000000000 ) ;
#3848=EDGE_LOOP ( 'NONE', ( #2770, #9341, #11773, #16373, #1649, #11112, #13691, #8113, #705, #11323, #13035, #3217, #13153, #15971, #14260, #2801 ) ) ;
#3859=CARTESIAN_POINT ( 'NONE',  ( 31.00000000000000711, 0.000000000000000000, -30.99999999999999289 ) ) ;
#3895=ORIENTED_EDGE ( 'NONE', *, *, #540, .T. ) ;
#3902=LINE ( 'NONE', #8898, #4670 ) ;
#3915=VECTOR ( 'NONE', #7529, 1000.000000000000000 ) ;
#3918=CARTESIAN_POINT ( 'NONE',  ( 26.00000000000000711, 68.00000000000000000, -31.00000000000002487 ) ) ;
#3967=EDGE_CURVE ( 'NONE', #9064, #7586, #2413, .T. ) ;
#3974=DIRECTION ( 'NONE',  ( 0.000000000000000000, 0.000000000000000000, -1.000000000000000000 ) ) ;
#3982=EDGE_LOOP ( 'NONE', ( #13146, #5828, #1714, #7225 ) ) ;
#3994=CYLINDRICAL_SURFACE ( 'NONE', #15450, 8.000000000000000000 ) ;
#4010=DIRECTION ( 'NONE',  ( -0.000000000000000000, -1.000000000000000000, 0.000000000000000000 ) ) ;
#4040=EDGE_CURVE ( 'NONE', #15, #15508, #15157, .T. ) ;
#4042=ADVANCED_FACE ( 'NONE', ( #6521 ), #17, .T. ) ;
#4062=EDGE_CURVE ( 'NONE', #11045, #12540, #14449, .T. ) ;
#4065=CARTESIAN_POINT ( 'NONE',  ( -40.00000000000000000, 0.000000000000000000, 26.00000000000000355 ) ) ;
#4076=VERTEX_POINT ( 'NONE', #9374 ) ;
#4080=AXIS2_PLACEMENT_3D ( 'NONE', #12166, #4271, #9506 ) ;
#4088=CARTESIAN_POINT ( 'NONE',  ( -37.00000000000000000, 68.00000000000000000, -22.99999999999999645 ) ) ;
#4110=CARTESIAN_POINT ( 'NONE',  ( -23.00000000000000000, 68.00000000000000000, -31.00000000000005684 ) ) ;
#4126=DIRECTION ( 'NONE',  ( -0.000000000000000000, -1.000000000000000000, -0.000000000000000000 ) ) ;
#4159=CARTESIAN_POINT ( 'NONE',  ( 25.99999999999999645, 68.00000000000000000, -39.99999999999999289 ) ) ;
#4175=CARTESIAN_POINT ( 'NONE',  ( -25.99999999999999645, 68.00000000000000000, -39.99999999999999289 ) ) ;
#4196=DIRECTION ( 'NONE',  ( 1.000000000000000000, 0.000000000000000000, -0.000000000000000000 ) ) ;
#4199=AXIS2_PLACEMENT_3D ( 'NONE', #14036, #11709, #16768 ) ;
#4206=PRODUCT_DEFINITION_CONTEXT ( 'detailed design', #15862, 'design' ) ;
#4210=VERTEX_POINT ( 'NONE', #16407 ) ;
#4223=VERTEX_POINT ( 'NONE', #12377 ) ;
#4224=VERTEX_POINT ( 'NONE', #16327 ) ;
#4246=VERTEX_POINT ( 'NONE', #13673 ) ;
#4253=DIRECTION ( 'NONE',  ( 0.000000000000000000, 0.000000000000000000, -1.000000000000000000 ) ) ;
#4264=EDGE_CURVE ( 'NONE', #15448, #4076, #3530, .T. ) ;
#4269=DIRECTION ( 'NONE',  ( 0.000000000000000000, -1.000000000000000000, 0.000000000000000000 ) ) ;
#4271=DIRECTION ( 'NONE',  ( -0.000000000000000000, -1.000000000000000000, 0.000000000000000000 ) ) ;
#4273=CARTESIAN_POINT ( 'NONE',  ( -22.99999999999999645, 68.00000000000000000, -36.99999999999999289 ) ) ;
#4286=AXIS2_PLACEMENT_3D ( 'NONE', #7464, #11348, #10073 ) ;
#4295=DIRECTION ( 'NONE',  ( -0.000000000000000000, -1.000000000000000000, -0.000000000000000000 ) ) ;
#4316=VERTEX_POINT ( 'NONE', #8601 ) ;
#4325=AXIS2_PLACEMENT_3D ( 'NONE', #14015, #6015, #12478 ) ;
#4344=ORIENTED_EDGE ( 'NONE', *, *, #14710, .F. ) ;
#4354=LINE ( 'NONE', #8204, #2158 ) ;
#4365=DIRECTION ( 'NONE',  ( 0.000000000000000000, 0.000000000000000000, -1.000000000000000000 ) ) ;
#4372=ADVANCED_FACE ( 'NONE', ( #11503 ), #12961, .F. ) ;
#4433=DIRECTION ( 'NONE',  ( 0.000000000000000000, 0.000000000000000000, -1.000000000000000000 ) ) ;
#4453=DIRECTION ( 'NONE',  ( 1.000000000000000000, -0.000000000000000000, 0.000000000000000000 ) ) ;
#4473=DIRECTION ( 'NONE',  ( -1.000000000000000000, 0.000000000000000000, 7.709882115452498874E-16 ) ) ;
#4479=CARTESIAN_POINT ( 'NONE',  ( -37.00000000000000000, 0.000000000000000000, 23.00000000000000355 ) ) ;
#4492=ORIENTED_EDGE ( 'NONE', *, *, #15269, .T. ) ;
#4515=AXIS2_PLACEMENT_3D ( 'NONE', #12716, #13058, #16818 ) ;
#4540=LINE ( 'NONE', #13808, #16092 ) ;
#4621=EDGE_LOOP ( 'NONE', ( #16042, #3729, #7588, #3144, #6974, #8590, #6421, #4492, #16854, #2631, #14538, #14321, #82, #5685, #15113, #11003 ) ) ;
#4645=AXIS2_PLACEMENT_3D ( 'NONE', #6771, #1711, #5743 ) ;
#4669=FACE_OUTER_BOUND ( 'NONE', #16405, .T. ) ;
#4670=VECTOR ( 'NONE', #4925, 1000.000000000000000 ) ;
#4689=EDGE_CURVE ( 'NONE', #15644, #4224, #10562, .T. ) ;
#4702=CARTESIAN_POINT ( 'NONE',  ( 31.00000000000002842, 68.00000000000000000, 26.00000000000001066 ) ) ;
#4736=VERTEX_POINT ( 'NONE', #8578 ) ;
#4749=VECTOR ( 'NONE', #3303, 1000.000000000000000 ) ;
#4753=ORIENTED_EDGE ( 'NONE', *, *, #1204, .T. ) ;
#4764=VECTOR ( 'NONE', #14535, 1000.000000000000000 ) ;
#4786=CARTESIAN_POINT ( 'NONE',  ( -25.99999999999999645, 0.000000000000000000, -31.00000000000003197 ) ) ;
#4812=VECTOR ( 'NONE', #3592, 1000.000000000000000 ) ;
#4815=ORIENTED_EDGE ( 'NONE', *, *, #15609, .F. ) ;
#4830=EDGE_CURVE ( 'NONE', #11889, #2294, #6394, .T. ) ;
#4867=EDGE_CURVE ( 'NONE', #11960, #10491, #15353, .T. ) ;
#4870=ORIENTED_EDGE ( 'NONE', *, *, #3967, .T. ) ;
#4887=EDGE_CURVE ( 'NONE', #12156, #5336, #4947, .T. ) ;
#4898=LINE ( 'NONE', #2402, #15417 ) ;
#4917=DIRECTION ( 'NONE',  ( 1.000000000000000000, 0.000000000000000000, 0.000000000000000000 ) ) ;
#4925=DIRECTION ( 'NONE',  ( -0.000000000000000000, -1.000000000000000000, -0.000000000000000000 ) ) ;
#4927=ORIENTED_EDGE ( 'NONE', *, *, #16170, .F. ) ;
#4931=DIRECTION ( 'NONE',  ( -1.000000000000000000, 0.000000000000000000, -0.000000000000000000 ) ) ;
#4947=LINE ( 'NONE', #13589, #13324 ) ;
#4960=ORIENTED_EDGE ( 'NONE', *, *, #2791, .F. ) ;
#4981=VERTEX_POINT ( 'NONE', #2633 ) ;
#5008=LINE ( 'NONE', #10174, #16808 ) ;
#5063=CARTESIAN_POINT ( 'NONE',  ( 22.99999999999999289, 68.00000000000000000, 37.00000000000002132 ) ) ;
#5070=ORIENTED_EDGE ( 'NONE', *, *, #11399, .T. ) ;
#5079=ORIENTED_EDGE ( 'NONE', *, *, #15759, .F. ) ;
#5099=EDGE_CURVE ( 'NONE', #10491, #3758, #13879, .T. ) ;
#5106=CARTESIAN_POINT ( 'NONE',  ( -31.00000000000003197, 0.000000000000000000, -22.99999999999999645 ) ) ;
#5119=EDGE_LOOP ( 'NONE', ( #7382, #15872, #14797, #10354 ) ) ;
#5151=EDGE_LOOP ( 'NONE', ( #32, #6064, #9289, #14099 ) ) ;
#5156=EDGE_CURVE ( 'NONE', #10758, #10732, #16290, .T. ) ;
#5255=CARTESIAN_POINT ( 'NONE',  ( -37.00000000000000000, 0.000000000000000000, -22.99999999999999645 ) ) ;
#5256=ORIENTED_EDGE ( 'NONE', *, *, #189, .F. ) ;
#5299=PLANE ( 'NONE',  #841 ) ;
#5314=CIRCLE ( 'NONE', #12464, 4.999999999999997335 ) ;
#5319=AXIS2_PLACEMENT_3D ( 'NONE', #8870, #11775, #11862 ) ;
#5323=LINE ( 'NONE', #3790, #8789 ) ;
#5334=AXIS2_PLACEMENT_3D ( 'NONE', #2042, #3085, #8417 ) ;
#5336=VERTEX_POINT ( 'NONE', #3657 ) ;
#5349=VERTEX_POINT ( 'NONE', #10273 ) ;
#5374=ORIENTED_EDGE ( 'NONE', *, *, #4689, .F. ) ;
#5405=ADVANCED_FACE ( 'NONE', ( #14385 ), #2870, .F. ) ;
#5421=VERTEX_POINT ( 'NONE', #4159 ) ;
#5427=ADVANCED_FACE ( 'NONE', ( #2616 ), #304, .F. ) ;
#5435=EDGE_LOOP ( 'NONE', ( #9938, #10852, #14677, #1768, #6280, #15825, #634, #12462, #931, #6446, #7362, #11820, #14365, #4815, #5951, #16883 ) ) ;
#5439=CARTESIAN_POINT ( 'NONE',  ( 31.00000000000000711, 68.00000000000000000, -30.99999999999999289 ) ) ;
#5444=( NAMED_UNIT ( * ) PLANE_ANGLE_UNIT ( ) SI_UNIT ( $, .RADIAN. ) );
#5462=EDGE_LOOP ( 'NONE', ( #3826, #938, #4927, #13393 ) ) ;
#5474=ORIENTED_EDGE ( 'NONE', *, *, #3121, .T. ) ;
#5507=LINE ( 'NONE', #11782, #11093 ) ;
#5510=DIRECTION ( 'NONE',  ( 0.000000000000000000, 0.000000000000000000, 1.000000000000000000 ) ) ;
#5520=EDGE_CURVE ( 'NONE', #15647, #2162, #8194, .T. ) ;
#5524=EDGE_CURVE ( 'NONE', #9064, #11889, #1844, .T. ) ;
#5528=ORIENTED_EDGE ( 'NONE', *, *, #4830, .F. ) ;
#5531=DIRECTION ( 'NONE',  ( -0.000000000000000000, -1.000000000000000000, -0.000000000000000000 ) ) ;
#5544=ORIENTED_EDGE ( 'NONE', *, *, #373, .F. ) ;
#5551=CARTESIAN_POINT ( 'NONE',  ( -30.99999999999999289, 68.00000000000000000, 31.00000000000000000 ) ) ;
#5576=EDGE_CURVE ( 'NONE', #2891, #10664, #14815, .T. ) ;
#5600=LINE ( 'NONE', #10671, #3148 ) ;
#5652=FACE_OUTER_BOUND ( 'NONE', #5462, .T. ) ;
#5659=ORIENTED_EDGE ( 'NONE', *, *, #170, .F. ) ;
#5675=FACE_OUTER_BOUND ( 'NONE', #11686, .T. ) ;
#5681=ORIENTED_EDGE ( 'NONE', *, *, #14624, .F. ) ;
#5685=ORIENTED_EDGE ( 'NONE', *, *, #809, .T. ) ;
#5702=DIRECTION ( 'NONE',  ( -0.000000000000000000, -0.000000000000000000, 1.000000000000000000 ) ) ;
#5719=CIRCLE ( 'NONE', #4080, 8.000000000000000000 ) ;
#5743=DIRECTION ( 'NONE',  ( 0.000000000000000000, 0.000000000000000000, -1.000000000000000000 ) ) ;
#5746=AXIS2_PLACEMENT_3D ( 'NONE', #6090, #11341, #16585 ) ;
#5773=CARTESIAN_POINT ( 'NONE',  ( 40.00000000000000000, 68.00000000000000000, 26.00000000000000355 ) ) ;
#5787=CARTESIAN_POINT ( 'NONE',  ( -37.00000000000000000, 0.000000000000000000, -22.99999999999999645 ) ) ;
#5810=VECTOR ( 'NONE', #4295, 1000.000000000000000 ) ;
#5828=ORIENTED_EDGE ( 'NONE', *, *, #11399, .F. ) ;
#5843=SHAPE_REPRESENTATION ( 'Servo-Body', ( #1488 ), #3145 ) ;
#5852=VERTEX_POINT ( 'NONE', #3186 ) ;
#5855=VECTOR ( 'NONE', #719, 1000.000000000000000 ) ;
#5909=LINE ( 'NONE', #4786, #16394 ) ;
#5913=VECTOR ( 'NONE', #6984, 1000.000000000000000 ) ;
#5915=LINE ( 'NONE', #4702, #3915 ) ;
#5951=ORIENTED_EDGE ( 'NONE', *, *, #6579, .F. ) ;
#6015=DIRECTION ( 'NONE',  ( -0.000000000000000000, -1.000000000000000000, 0.000000000000000000 ) ) ;
#6017=VECTOR ( 'NONE', #3400, 1000.000000000000000 ) ;
#6051=DIRECTION ( 'NONE',  ( -1.000000000000000000, 0.000000000000000000, -0.000000000000000000 ) ) ;
#6055=UNCERTAINTY_MEASURE_WITH_UNIT (LENGTH_MEASURE( 1.000000000000000082E-05 ), #1412, 'distance_accuracy_value', 'NONE');
#6063=LINE ( 'NONE', #16553, #9554 ) ;
#6064=ORIENTED_EDGE ( 'NONE', *, *, #9828, .F. ) ;
#6079=ORIENTED_EDGE ( 'NONE', *, *, #6742, .F. ) ;
#6080=EDGE_CURVE ( 'NONE', #12484, #14967, #8221, .T. ) ;
#6088=PRODUCT_CONTEXT ( 'NONE', #10935, 'mechanical' ) ;
#6090=CARTESIAN_POINT ( 'NONE',  ( -22.99999999999999645, 68.00000000000000000, 37.00000000000002132 ) ) ;
#6091=ORIENTED_EDGE ( 'NONE', *, *, #4867, .T. ) ;
#6120=CARTESIAN_POINT ( 'NONE',  ( 31.00000000000002842, 68.00000000000000000, 23.00000000000001066 ) ) ;
#6126=AXIS2_PLACEMENT_3D ( 'NONE', #2325, #14265, #1376 ) ;
#6158=ORIENTED_EDGE ( 'NONE', *, *, #4887, .F. ) ;
#6177=ORIENTED_EDGE ( 'NONE', *, *, #15524, .F. ) ;
#6195=LINE ( 'NONE', #10085, #15728 ) ;
#6198=DIRECTION ( 'NONE',  ( 1.000000000000000000, 0.000000000000000000, 0.000000000000000000 ) ) ;
#6208=CARTESIAN_POINT ( 'NONE',  ( -37.00000000000000000, 68.00000000000000000, 23.00000000000000355 ) ) ;
#6210=ORIENTED_EDGE ( 'NONE', *, *, #5156, .F. ) ;
#6226=CARTESIAN_POINT ( 'NONE',  ( 31.00000000000004263, 0.000000000000000000, -25.99999999999999645 ) ) ;
#6261=DIRECTION ( 'NONE',  ( 1.000000000000000000, 0.000000000000000000, 0.000000000000000000 ) ) ;
#6280=ORIENTED_EDGE ( 'NONE', *, *, #15293, .F. ) ;
#6285=DIRECTION ( 'NONE',  ( 0.000000000000000000, 0.000000000000000000, -1.000000000000000000 ) ) ;
#6319=VERTEX_POINT ( 'NONE', #8817 ) ;
#6333=CARTESIAN_POINT ( 'NONE',  ( -37.00000000000000000, 0.000000000000000000, 23.00000000000000355 ) ) ;
#6343=( GEOMETRIC_REPRESENTATION_CONTEXT ( 3 ) GLOBAL_UNCERTAINTY_ASSIGNED_CONTEXT ( ( #6055 ) ) GLOBAL_UNIT_ASSIGNED_CONTEXT ( ( #1412, #5444, #16102 ) ) REPRESENTATION_CONTEXT ( 'NONE', 'WORKASPACE' ) );
#6365=ORIENTED_EDGE ( 'NONE', *, *, #11263, .F. ) ;
#6368=VERTEX_POINT ( 'NONE', #10502 ) ;
#6394=LINE ( 'NONE', #9079, #8393 ) ;
#6416=ORIENTED_EDGE ( 'NONE', *, *, #15759, .T. ) ;
#6421=ORIENTED_EDGE ( 'NONE', *, *, #10334, .T. ) ;
#6425=EDGE_LOOP ( 'NONE', ( #9219, #6177, #420, #11819 ) ) ;
#6427=DIRECTION ( 'NONE',  ( 1.000000000000000000, 0.000000000000000000, -0.000000000000000000 ) ) ;
#6441=CIRCLE ( 'NONE', #4286, 4.999999999999997335 ) ;
#6446=ORIENTED_EDGE ( 'NONE', *, *, #6660, .F. ) ;
#6476=LINE ( 'NONE', #6226, #11037 ) ;
#6486=DIRECTION ( 'NONE',  ( -0.000000000000000000, -1.000000000000000000, -0.000000000000000000 ) ) ;
#6496=CARTESIAN_POINT ( 'NONE',  ( 31.00000000000002842, 0.000000000000000000, 23.00000000000001066 ) ) ;
#6521=FACE_OUTER_BOUND ( 'NONE', #5119, .T. ) ;
#6526=ADVANCED_FACE ( 'NONE', ( #10757 ), #13351, .F. ) ;
#6538=EDGE_LOOP ( 'NONE', ( #13448, #1534, #15758, #13758 ) ) ;
#6579=EDGE_CURVE ( 'NONE', #1698, #14192, #8613, .T. ) ;
#6609=VECTOR ( 'NONE', #14254, 1000.000000000000000 ) ;
#6615=ORIENTED_EDGE ( 'NONE', *, *, #15781, .F. ) ;
#6626=MECHANICAL_DESIGN_GEOMETRIC_PRESENTATION_REPRESENTATION('',(#8568),#6343);
#6639=LINE ( 'NONE', #15927, #14594 ) ;
#6651=VERTEX_POINT ( 'NONE', #3623 ) ;
#6659=EDGE_CURVE ( 'NONE', #4981, #14719, #6441, .T. ) ;
#6660=EDGE_CURVE ( 'NONE', #12540, #15586, #2078, .T. ) ;
#6671=AXIS2_PLACEMENT_3D ( 'NONE', #13456, #4269, #9502 ) ;
#6697=PLANE ( 'NONE',  #3491 ) ;
#6700=DIRECTION ( 'NONE',  ( 0.000000000000000000, 0.000000000000000000, -1.000000000000000000 ) ) ;
#6702=EDGE_CURVE ( 'NONE', #6319, #13922, #12500, .T. ) ;
#6721=LINE ( 'NONE', #11975, #12001 ) ;
#6722=CARTESIAN_POINT ( 'NONE',  ( -30.99999999999999645, 68.00000000000000000, -30.99999999999999289 ) ) ;
#6730=SURFACE_STYLE_FILL_AREA ( #2704 ) ;
#6742=EDGE_CURVE ( 'NONE', #13922, #12156, #12981, .T. ) ;
#6758=PLANE ( 'NONE',  #7400 ) ;
#6762=ADVANCED_FACE ( 'NONE', ( #8948 ), #6697, .T. ) ;
#6771=CARTESIAN_POINT ( 'NONE',  ( -30.99999999999999645, 0.000000000000000000, -30.99999999999999289 ) ) ;
#6819=LINE ( 'NONE', #4175, #11429 ) ;
#6824=ORIENTED_EDGE ( 'NONE', *, *, #11517, .F. ) ;
#6838=LINE ( 'NONE', #8313, #16237 ) ;
#6854=CARTESIAN_POINT ( 'NONE',  ( 31.00000000000004263, 68.00000000000000000, -25.99999999999999645 ) ) ;
#6862=CARTESIAN_POINT ( 'NONE',  ( -30.99999999999999645, 68.00000000000000000, -30.99999999999999289 ) ) ;
#6864=ORIENTED_EDGE ( 'NONE', *, *, #16335, .F. ) ;
#6873=ADVANCED_FACE ( 'NONE', ( #5675 ), #16152, .F. ) ;
#6884=CARTESIAN_POINT ( 'NONE',  ( -30.99999999999999289, 68.00000000000000000, 31.00000000000000000 ) ) ;
#6897=EDGE_CURVE ( 'NONE', #10732, #8165, #10833, .T. ) ;
#6908=CARTESIAN_POINT ( 'NONE',  ( 31.00000000000000711, 68.00000000000000000, -30.99999999999999289 ) ) ;
#6911=LINE ( 'NONE', #12171, #1094 ) ;
#6921=ORIENTED_EDGE ( 'NONE', *, *, #3967, .F. ) ;
#6922=CARTESIAN_POINT ( 'NONE',  ( -37.00000000000000000, 68.00000000000000000, -22.99999999999999645 ) ) ;
#6942=VERTEX_POINT ( 'NONE', #11952 ) ;
#6968=CYLINDRICAL_SURFACE ( 'NONE', #8347, 8.000000000000000000 ) ;
#6970=VERTEX_POINT ( 'NONE', #1891 ) ;
#6974=ORIENTED_EDGE ( 'NONE', *, *, #10767, .T. ) ;
#6982=EDGE_CURVE ( 'NONE', #6651, #6970, #528, .T. ) ;
#6984=DIRECTION ( 'NONE',  ( -0.000000000000000000, -1.000000000000000000, -0.000000000000000000 ) ) ;
#6991=DIRECTION ( 'NONE',  ( -0.000000000000000000, -0.000000000000000000, 1.000000000000000000 ) ) ;
#6999=LINE ( 'NONE', #4273, #16786 ) ;
#7014=VECTOR ( 'NONE', #5702, 1000.000000000000000 ) ;
#7026=CARTESIAN_POINT ( 'NONE',  ( 25.99999999999999645, 68.00000000000000000, 40.00000000000002132 ) ) ;
#7070=EDGE_CURVE ( 'NONE', #9593, #10447, #16570, .T. ) ;
#7128=VECTOR ( 'NONE', #3653, 1000.000000000000000 ) ;
#7161=CARTESIAN_POINT ( 'NONE',  ( 40.00000000000000000, 0.000000000000000000, 26.00000000000000355 ) ) ;
#7179=EDGE_CURVE ( 'NONE', #14967, #1326, #9267, .T. ) ;
#7210=( NAMED_UNIT ( * ) PLANE_ANGLE_UNIT ( ) SI_UNIT ( $, .RADIAN. ) );
#7225=ORIENTED_EDGE ( 'NONE', *, *, #3012, .T. ) ;
#7226=ORIENTED_EDGE ( 'NONE', *, *, #15374, .F. ) ;
#7285=PLANE ( 'NONE',  #12195 ) ;
#7297=SHAPE_DEFINITION_REPRESENTATION ( #10980, #5843 ) ;
#7306=EDGE_CURVE ( 'NONE', #10664, #7586, #8145, .T. ) ;
#7322=DIRECTION ( 'NONE',  ( 0.000000000000000000, 0.000000000000000000, -1.000000000000000000 ) ) ;
#7323=CARTESIAN_POINT ( 'NONE',  ( 37.00000000000000000, 0.000000000000000000, 23.00000000000001066 ) ) ;
#7359=ORIENTED_EDGE ( 'NONE', *, *, #15291, .T. ) ;
#7362=ORIENTED_EDGE ( 'NONE', *, *, #4062, .F. ) ;
#7382=ORIENTED_EDGE ( 'NONE', *, *, #10974, .F. ) ;
#7384=CARTESIAN_POINT ( 'NONE',  ( -22.99999999999999645, 68.00000000000000000, 37.00000000000002132 ) ) ;
#7400=AXIS2_PLACEMENT_3D ( 'NONE', #12094, #9606, #9528 ) ;
#7417=PLANE ( 'NONE',  #9382 ) ;
#7426=DIRECTION ( 'NONE',  ( 0.000000000000000000, 0.000000000000000000, 1.000000000000000000 ) ) ;
#7442=EDGE_LOOP ( 'NONE', ( #4344, #6864, #14932, #11871 ) ) ;
#7457=EDGE_CURVE ( 'NONE', #2891, #9064, #4540, .T. ) ;
#7464=CARTESIAN_POINT ( 'NONE',  ( -30.99999999999999289, 68.00000000000000000, 31.00000000000000000 ) ) ;
#7506=DIRECTION ( 'NONE',  ( 0.000000000000000000, 0.000000000000000000, -1.000000000000000000 ) ) ;
#7529=DIRECTION ( 'NONE',  ( 1.000000000000000000, 0.000000000000000000, -7.709882115452498874E-16 ) ) ;
#7548=CARTESIAN_POINT ( 'NONE',  ( -25.99999999999999645, 0.000000000000000000, -31.00000000000003197 ) ) ;
#7556=DIRECTION ( 'NONE',  ( -1.000000000000000000, -0.000000000000000000, -0.000000000000000000 ) ) ;
#7586=VERTEX_POINT ( 'NONE', #2536 ) ;
#7588=ORIENTED_EDGE ( 'NONE', *, *, #13617, .T. ) ;
#7640=CARTESIAN_POINT ( 'NONE',  ( 37.00000000000000000, 0.000000000000000000, 23.00000000000001066 ) ) ;
#7642=EDGE_LOOP ( 'NONE', ( #4753, #6210, #9112, #2953 ) ) ;
#7668=FACE_OUTER_BOUND ( 'NONE', #13947, .T. ) ;
#7697=CARTESIAN_POINT ( 'NONE',  ( 31.00000000000004263, 68.00000000000000000, -25.99999999999999645 ) ) ;
#7700=EDGE_CURVE ( 'NONE', #5421, #15647, #6819, .T. ) ;
#7712=ORIENTED_EDGE ( 'NONE', *, *, #7306, .T. ) ;
#7716=DIRECTION ( 'NONE',  ( -0.000000000000000000, -1.000000000000000000, -0.000000000000000000 ) ) ;
#7750=VECTOR ( 'NONE', #4917, 1000.000000000000000 ) ;
#7754=EDGE_CURVE ( 'NONE', #2083, #10758, #9798, .T. ) ;
#7807=FACE_BOUND ( 'NONE', #4621, .T. ) ;
#7811=FACE_OUTER_BOUND ( 'NONE', #15753, .T. ) ;
#7816=ORIENTED_EDGE ( 'NONE', *, *, #9415, .T. ) ;
#7839=ORIENTED_EDGE ( 'NONE', *, *, #1223, .T. ) ;
#7840=AXIS2_PLACEMENT_3D ( 'NONE', #191, #12117, #4473 ) ;
#7869=LINE ( 'NONE', #11826, #15437 ) ;
#7890=PLANE ( 'NONE',  #346 ) ;
#7941=DIRECTION ( 'NONE',  ( -1.000000000000000000, -0.000000000000000000, -0.000000000000000000 ) ) ;
#7961=FACE_OUTER_BOUND ( 'NONE', #11711, .T. ) ;
#7980=CARTESIAN_POINT ( 'NONE',  ( 23.00000000000000711, 68.00000000000000000, -31.00000000000002487 ) ) ;
#7982=LINE ( 'NONE', #11955, #2856 ) ;
#7984=VERTEX_POINT ( 'NONE', #12910 ) ;
#7996=DIRECTION ( 'NONE',  ( -0.000000000000000000, -0.000000000000000000, 1.000000000000000000 ) ) ;
#8012=EDGE_LOOP ( 'NONE', ( #2001, #2224, #3128, #13466 ) ) ;
#8030=DIRECTION ( 'NONE',  ( 0.000000000000000000, 0.000000000000000000, -1.000000000000000000 ) ) ;
#8057=DIRECTION ( 'NONE',  ( 5.782411586589399054E-16, 0.000000000000000000, -1.000000000000000000 ) ) ;
#8059=LINE ( 'NONE', #172, #2544 ) ;
#8071=UNCERTAINTY_MEASURE_WITH_UNIT (LENGTH_MEASURE( 1.000000000000000082E-05 ), #8513, 'distance_accuracy_value', 'NONE');
#8082=ORIENTED_EDGE ( 'NONE', *, *, #10790, .T. ) ;
#8110=DIRECTION ( 'NONE',  ( -0.000000000000000000, -1.000000000000000000, -0.000000000000000000 ) ) ;
#8113=ORIENTED_EDGE ( 'NONE', *, *, #6659, .T. ) ;
#8145=LINE ( 'NONE', #8224, #12523 ) ;
#8165=VERTEX_POINT ( 'NONE', #13266 ) ;
#8179=CARTESIAN_POINT ( 'NONE',  ( 40.00000000000000000, 0.000000000000000000, 26.00000000000000355 ) ) ;
#8194=LINE ( 'NONE', #8375, #7014 ) ;
#8202=PLANE ( 'NONE',  #6671 ) ;
#8204=CARTESIAN_POINT ( 'NONE',  ( 40.00000000000000000, 68.00000000000000000, 26.00000000000000355 ) ) ;
#8213=EDGE_CURVE ( 'NONE', #13922, #4246, #6721, .T. ) ;
#8218=CARTESIAN_POINT ( 'NONE',  ( 30.99999999999999645, 68.00000000000000000, 31.00000000000001066 ) ) ;
#8221=LINE ( 'NONE', #13476, #1548 ) ;
#8223=PLANE ( 'NONE',  #13 ) ;
#8224=CARTESIAN_POINT ( 'NONE',  ( -40.00000000000000000, 0.000000000000000000, -25.99999999999999645 ) ) ;
#8277=VECTOR ( 'NONE', #8057, 1000.000000000000000 ) ;
#8303=CIRCLE ( 'NONE', #902, 5.000000000000000888 ) ;
#8313=CARTESIAN_POINT ( 'NONE',  ( -31.00000000000003197, 68.00000000000000000, -22.99999999999999645 ) ) ;
#8343=ORIENTED_EDGE ( 'NONE', *, *, #6982, .F. ) ;
#8347=AXIS2_PLACEMENT_3D ( 'NONE', #3206, #3284, #2073 ) ;
#8375=CARTESIAN_POINT ( 'NONE',  ( -25.99999999999999645, 68.00000000000000000, -31.00000000000003197 ) ) ;
#8393=VECTOR ( 'NONE', #14065, 1000.000000000000000 ) ;
#8396=ORIENTED_EDGE ( 'NONE', *, *, #15755, .T. ) ;
#8400=LINE ( 'NONE', #16375, #11565 ) ;
#8417=DIRECTION ( 'NONE',  ( 0.000000000000000000, 0.000000000000000000, -1.000000000000000000 ) ) ;
#8513=( LENGTH_UNIT ( ) NAMED_UNIT ( * ) SI_UNIT ( .MILLI., .METRE. ) );
#8551=EDGE_CURVE ( 'NONE', #4736, #10866, #5909, .T. ) ;
#8555=DIRECTION ( 'NONE',  ( 0.000000000000000000, 0.000000000000000000, -1.000000000000000000 ) ) ;
#8560=DIRECTION ( 'NONE',  ( -1.000000000000000000, -0.000000000000000000, -0.000000000000000000 ) ) ;
#8561=EDGE_CURVE ( 'NONE', #9920, #16153, #6063, .T. ) ;
#8568=STYLED_ITEM ( 'NONE', ( #10867 ), #14168 ) ;
#8578=CARTESIAN_POINT ( 'NONE',  ( -25.99999999999999645, 0.000000000000000000, -39.99999999999999289 ) ) ;
#8590=ORIENTED_EDGE ( 'NONE', *, *, #4264, .T. ) ;
#8601=CARTESIAN_POINT ( 'NONE',  ( -31.00000000000005684, 68.00000000000000000, 23.00000000000000355 ) ) ;
#8613=LINE ( 'NONE', #15226, #11708 ) ;
#8644=CARTESIAN_POINT ( 'NONE',  ( 31.00000000000002842, 68.00000000000000000, 23.00000000000001066 ) ) ;
#8693=DIRECTION ( 'NONE',  ( 0.000000000000000000, 0.000000000000000000, 1.000000000000000000 ) ) ;
#8710=AXIS2_PLACEMENT_3D ( 'NONE', #5773, #14721, #5510 ) ;
#8745=DIRECTION ( 'NONE',  ( 1.000000000000000000, 0.000000000000000000, 0.000000000000000000 ) ) ;
#8774=EDGE_CURVE ( 'NONE', #11045, #5852, #8919, .T. ) ;
#8775=CARTESIAN_POINT ( 'NONE',  ( 26.00000000000001066, 0.000000000000000000, -31.00000000000002487 ) ) ;
#8789=VECTOR ( 'NONE', #7716, 1000.000000000000000 ) ;
#8790=ORIENTED_EDGE ( 'NONE', *, *, #9080, .T. ) ;
#8806=PLANE ( 'NONE',  #12089 ) ;
#8817=CARTESIAN_POINT ( 'NONE',  ( 31.00000000000006395, 68.00000000000000000, -22.99999999999999289 ) ) ;
#8839=CARTESIAN_POINT ( 'NONE',  ( -22.99999999999999645, 68.00000000000000000, 37.00000000000002132 ) ) ;
#8870=CARTESIAN_POINT ( 'NONE',  ( 31.00000000000000711, 68.00000000000000000, -30.99999999999999289 ) ) ;
#8898=CARTESIAN_POINT ( 'NONE',  ( -31.00000000000003197, 68.00000000000000000, 26.00000000000000355 ) ) ;
#8906=PLANE ( 'NONE',  #3593 ) ;
#8907=DIRECTION ( 'NONE',  ( 1.000000000000000000, 0.000000000000000000, -0.000000000000000000 ) ) ;
#8919=LINE ( 'NONE', #10197, #1645 ) ;
#8927=EDGE_CURVE ( 'NONE', #4210, #16153, #6911, .T. ) ;
#8948=FACE_OUTER_BOUND ( 'NONE', #1729, .T. ) ;
#8958=EDGE_CURVE ( 'NONE', #16701, #15, #9591, .T. ) ;
#8963=CARTESIAN_POINT ( 'NONE',  ( -25.99999999999999645, 68.00000000000000000, -39.99999999999999289 ) ) ;
#8977=FACE_OUTER_BOUND ( 'NONE', #11169, .T. ) ;
#9006=CARTESIAN_POINT ( 'NONE',  ( 30.99999999999999645, 0.000000000000000000, 31.00000000000001066 ) ) ;
#9010=CARTESIAN_POINT ( 'NONE',  ( -40.00000000000000000, 0.000000000000000000, 26.00000000000000355 ) ) ;
#9026=FACE_OUTER_BOUND ( 'NONE', #1040, .T. ) ;
#9032=DIRECTION ( 'NONE',  ( 0.000000000000000000, 0.000000000000000000, 1.000000000000000000 ) ) ;
#9038=DIRECTION ( 'NONE',  ( -0.000000000000000000, -1.000000000000000000, -0.000000000000000000 ) ) ;
#9064=VERTEX_POINT ( 'NONE', #1935 ) ;
#9073=CARTESIAN_POINT ( 'NONE',  ( -25.99999999999999645, 68.00000000000000000, 40.00000000000002132 ) ) ;
#9075=EDGE_LOOP ( 'NONE', ( #2872, #9237, #15660, #13157 ) ) ;
#9079=CARTESIAN_POINT ( 'NONE',  ( -40.00000000000000000, 68.00000000000000000, 26.00000000000000355 ) ) ;
#9080=EDGE_CURVE ( 'NONE', #4316, #11045, #14278, .T. ) ;
#9098=EDGE_CURVE ( 'NONE', #9930, #14326, #1242, .T. ) ;
#9102=EDGE_CURVE ( 'NONE', #4981, #15644, #3902, .T. ) ;
#9106=AXIS2_PLACEMENT_3D ( 'NONE', #16678, #640, #7322 ) ;
#9108=DIRECTION ( 'NONE',  ( -1.000000000000000000, 0.000000000000000000, -5.782411586589400040E-16 ) ) ;
#9110=VECTOR ( 'NONE', #1252, 1000.000000000000000 ) ;
#9112=ORIENTED_EDGE ( 'NONE', *, *, #7754, .F. ) ;
#9117=PLANE ( 'NONE',  #13553 ) ;
#9153=VECTOR ( 'NONE', #6991, 1000.000000000000000 ) ;
#9176=DIRECTION ( 'NONE',  ( -0.000000000000000000, -1.000000000000000000, 0.000000000000000000 ) ) ;
#9181=ADVANCED_FACE ( 'NONE', ( #8977 ), #14291, .F. ) ;
#9190=DIRECTION ( 'NONE',  ( -0.000000000000000000, -1.000000000000000000, 0.000000000000000000 ) ) ;
#9202=ADVANCED_FACE ( 'NONE', ( #1325 ), #8806, .T. ) ;
#9212=CARTESIAN_POINT ( 'NONE',  ( -22.99999999999999645, 68.00000000000000000, -31.00000000000005684 ) ) ;
#9219=ORIENTED_EDGE ( 'NONE', *, *, #8551, .T. ) ;
#9223=CARTESIAN_POINT ( 'NONE',  ( -25.99999999999999645, 0.000000000000000000, 40.00000000000002132 ) ) ;
#9233=DIRECTION ( 'NONE',  ( 0.000000000000000000, 0.000000000000000000, -1.000000000000000000 ) ) ;
#9237=ORIENTED_EDGE ( 'NONE', *, *, #8774, .F. ) ;
#9267=LINE ( 'NONE', #15540, #16349 ) ;
#9289=ORIENTED_EDGE ( 'NONE', *, *, #6659, .F. ) ;
#9299=DIRECTION ( 'NONE',  ( -0.000000000000000000, -0.000000000000000000, 1.000000000000000000 ) ) ;
#9310=FACE_OUTER_BOUND ( 'NONE', #5151, .T. ) ;
#9341=ORIENTED_EDGE ( 'NONE', *, *, #7700, .T. ) ;
#9349=LINE ( 'NONE', #15953, #8277 ) ;
#9361=LINE ( 'NONE', #6854, #16581 ) ;
#9374=CARTESIAN_POINT ( 'NONE',  ( -31.00000000000005684, 0.000000000000000000, 23.00000000000000355 ) ) ;
#9382=AXIS2_PLACEMENT_3D ( 'NONE', #11544, #16947, #4931 ) ;
#9389=ORIENTED_EDGE ( 'NONE', *, *, #5576, .F. ) ;
#9401=ORIENTED_EDGE ( 'NONE', *, *, #3050, .F. ) ;
#9415=EDGE_CURVE ( 'NONE', #16577, #15508, #5323, .T. ) ;
#9438=EDGE_CURVE ( 'NONE', #16577, #6651, #1293, .T. ) ;
#9462=ORIENTED_EDGE ( 'NONE', *, *, #2919, .F. ) ;
#9464=DIRECTION ( 'NONE',  ( -0.000000000000000000, -1.000000000000000000, 0.000000000000000000 ) ) ;
#9487=ORIENTED_EDGE ( 'NONE', *, *, #7700, .F. ) ;
#9502=DIRECTION ( 'NONE',  ( 0.000000000000000000, -0.000000000000000000, -1.000000000000000000 ) ) ;
#9506=DIRECTION ( 'NONE',  ( 0.000000000000000000, 0.000000000000000000, -1.000000000000000000 ) ) ;
#9528=DIRECTION ( 'NONE',  ( -1.000000000000000000, 0.000000000000000000, -0.000000000000000000 ) ) ;
#9531=AXIS2_PLACEMENT_3D ( 'NONE', #6908, #148, #8030 ) ;
#9554=VECTOR ( 'NONE', #9866, 1000.000000000000000 ) ;
#9556=AXIS2_PLACEMENT_3D ( 'NONE', #13778, #10086, #9914 ) ;
#9562=CARTESIAN_POINT ( 'NONE',  ( 25.99999999999999645, 68.00000000000000000, 40.00000000000002132 ) ) ;
#9591=LINE ( 'NONE', #8644, #6017 ) ;
#9593=VERTEX_POINT ( 'NONE', #11428 ) ;
#9606=DIRECTION ( 'NONE',  ( 0.000000000000000000, 0.000000000000000000, -1.000000000000000000 ) ) ;
#9654=ADVANCED_FACE ( 'NONE', ( #666 ), #500, .T. ) ;
#9728=DIRECTION ( 'NONE',  ( 1.000000000000000000, 0.000000000000000000, 0.000000000000000000 ) ) ;
#9731=ORIENTED_EDGE ( 'NONE', *, *, #8774, .T. ) ;
#9759=VECTOR ( 'NONE', #8555, 1000.000000000000000 ) ;
#9781=ORIENTED_EDGE ( 'NONE', *, *, #6080, .T. ) ;
#9798=CIRCLE ( 'NONE', #9531, 4.999999999999997335 ) ;
#9803=CARTESIAN_POINT ( 'NONE',  ( 26.00000000000000711, 68.00000000000000000, -31.00000000000002487 ) ) ;
#9818=ADVANCED_FACE ( 'NONE', ( #15257 ), #8906, .T. ) ;
#9828=EDGE_CURVE ( 'NONE', #14719, #4224, #10022, .T. ) ;
#9838=DIRECTION ( 'NONE',  ( -1.000000000000000000, 0.000000000000000000, -0.000000000000000000 ) ) ;
#9860=ORIENTED_EDGE ( 'NONE', *, *, #8958, .F. ) ;
#9865=PLANE ( 'NONE',  #3436 ) ;
#9866=DIRECTION ( 'NONE',  ( -0.000000000000000000, -1.000000000000000000, -0.000000000000000000 ) ) ;
#9880=CARTESIAN_POINT ( 'NONE',  ( -25.99999999999999645, 68.00000000000000000, 40.00000000000002132 ) ) ;
#9914=DIRECTION ( 'NONE',  ( 0.000000000000000000, 0.000000000000000000, -1.000000000000000000 ) ) ;
#9920=VERTEX_POINT ( 'NONE', #2621 ) ;
#9930=VERTEX_POINT ( 'NONE', #5106 ) ;
#9938=ORIENTED_EDGE ( 'NONE', *, *, #1417, .F. ) ;
#9949=VECTOR ( 'NONE', #11764, 1000.000000000000000 ) ;
#9958=EDGE_LOOP ( 'NONE', ( #1556, #6615, #9487, #2215 ) ) ;
#9991=CARTESIAN_POINT ( 'NONE',  ( 31.00000000000002842, 0.000000000000000000, 26.00000000000001066 ) ) ;
#10022=LINE ( 'NONE', #2193, #23 ) ;
#10059=ORIENTED_EDGE ( 'NONE', *, *, #3540, .F. ) ;
#10064=SHAPE_REPRESENTATION_RELATIONSHIP ( 'NONE' , 'NONE' ,  #5843, #11793 ) ;
#10073=DIRECTION ( 'NONE',  ( 0.000000000000000000, 0.000000000000000000, -1.000000000000000000 ) ) ;
#10085=CARTESIAN_POINT ( 'NONE',  ( -37.00000000000000000, 68.00000000000000000, 23.00000000000000355 ) ) ;
#10086=DIRECTION ( 'NONE',  ( -0.000000000000000000, -1.000000000000000000, -0.000000000000000000 ) ) ;
#10107=ADVANCED_FACE ( 'NONE', ( #13624 ), #16270, .T. ) ;
#10130=CARTESIAN_POINT ( 'NONE',  ( -25.99999999999999645, 68.00000000000000000, -31.00000000000003197 ) ) ;
#10172=ORIENTED_EDGE ( 'NONE', *, *, #8927, .T. ) ;
#10174=CARTESIAN_POINT ( 'NONE',  ( 31.00000000000006395, 0.000000000000000000, -22.99999999999999289 ) ) ;
#10177=DIRECTION ( 'NONE',  ( 1.000000000000000000, -0.000000000000000000, 0.000000000000000000 ) ) ;
#10189=CARTESIAN_POINT ( 'NONE',  ( 37.00000000000000000, 68.00000000000000000, 23.00000000000001066 ) ) ;
#10197=CARTESIAN_POINT ( 'NONE',  ( -22.99999999999999645, 68.00000000000000000, 31.00000000000003908 ) ) ;
#10201=AXIS2_PLACEMENT_3D ( 'NONE', #3859, #9190, #1453 ) ;
#10208=CIRCLE ( 'NONE', #15146, 8.000000000000000000 ) ;
#10211=CARTESIAN_POINT ( 'NONE',  ( -22.99999999999999645, 68.00000000000000000, -36.99999999999999289 ) ) ;
#10251=ORIENTED_EDGE ( 'NONE', *, *, #6579, .T. ) ;
#10253=DIRECTION ( 'NONE',  ( -0.000000000000000000, -1.000000000000000000, -0.000000000000000000 ) ) ;
#10254=VECTOR ( 'NONE', #12481, 1000.000000000000000 ) ;
#10255=AXIS2_PLACEMENT_3D ( 'NONE', #6120, #11122, #9838 ) ;
#10273=CARTESIAN_POINT ( 'NONE',  ( 30.99999999999999645, 68.00000000000000000, 26.00000000000001066 ) ) ;
#10286=LINE ( 'NONE', #3918, #14269 ) ;
#10309=VECTOR ( 'NONE', #6261, 1000.000000000000000 ) ;
#10334=EDGE_CURVE ( 'NONE', #4076, #5852, #15665, .T. ) ;
#10347=ORIENTED_EDGE ( 'NONE', *, *, #6897, .T. ) ;
#10349=DIRECTION ( 'NONE',  ( -1.000000000000000000, -0.000000000000000000, 1.156482317317883755E-15 ) ) ;
#10354=ORIENTED_EDGE ( 'NONE', *, *, #6742, .T. ) ;
#10397=EDGE_CURVE ( 'NONE', #14549, #9920, #12996, .T. ) ;
#10400=CARTESIAN_POINT ( 'NONE',  ( 23.00000000000000711, 0.000000000000000000, -31.00000000000002487 ) ) ;
#10411=ORIENTED_EDGE ( 'NONE', *, *, #15755, .F. ) ;
#10447=VERTEX_POINT ( 'NONE', #9223 ) ;
#10476=CARTESIAN_POINT ( 'NONE',  ( 26.00000000000001066, 68.00000000000000000, -31.00000000000002487 ) ) ;
#10491=VERTEX_POINT ( 'NONE', #8179 ) ;
#10497=DIRECTION ( 'NONE',  ( -0.000000000000000000, -1.000000000000000000, -0.000000000000000000 ) ) ;
#10502=CARTESIAN_POINT ( 'NONE',  ( 22.99999999999999645, 0.000000000000000000, 31.00000000000006750 ) ) ;
#10522=EDGE_CURVE ( 'NONE', #7586, #2294, #2854, .T. ) ;
#10549=FACE_OUTER_BOUND ( 'NONE', #12288, .T. ) ;
#10562=CIRCLE ( 'NONE', #5334, 4.999999999999997335 ) ;
#10634=DIRECTION ( 'NONE',  ( 1.000000000000000000, 0.000000000000000000, -0.000000000000000000 ) ) ;
#10654=CARTESIAN_POINT ( 'NONE',  ( 37.00000000000000000, 68.00000000000000000, -23.00000000000000000 ) ) ;
#10655=ORIENTED_EDGE ( 'NONE', *, *, #3324, .F. ) ;
#10664=VERTEX_POINT ( 'NONE', #12554 ) ;
#10671=CARTESIAN_POINT ( 'NONE',  ( -25.99999999999999645, 0.000000000000000000, 40.00000000000002132 ) ) ;
#10692=LINE ( 'NONE', #12246, #14362 ) ;
#10695=FACE_OUTER_BOUND ( 'NONE', #1054, .T. ) ;
#10708=CARTESIAN_POINT ( 'NONE',  ( -23.00000000000000000, 0.000000000000000000, -36.99999999999999289 ) ) ;
#10732=VERTEX_POINT ( 'NONE', #8775 ) ;
#10757=FACE_OUTER_BOUND ( 'NONE', #12463, .T. ) ;
#10758=VERTEX_POINT ( 'NONE', #10476 ) ;
#10764=FACE_OUTER_BOUND ( 'NONE', #13945, .T. ) ;
#10767=EDGE_CURVE ( 'NONE', #14326, #15448, #11507, .T. ) ;
#10790=EDGE_CURVE ( 'NONE', #15586, #3442, #4898, .T. ) ;
#10800=DIRECTION ( 'NONE',  ( -0.000000000000000000, -1.000000000000000000, -0.000000000000000000 ) ) ;
#10813=DIRECTION ( 'NONE',  ( 1.000000000000000000, 0.000000000000000000, 0.000000000000000000 ) ) ;
#10815=FACE_OUTER_BOUND ( 'NONE', #12061, .T. ) ;
#10825=ADVANCED_FACE ( 'NONE', ( #13143, #7807 ), #4, .T. ) ;
#10827=ADVANCED_FACE ( 'NONE', ( #9026 ), #7890, .T. ) ;
#10833=LINE ( 'NONE', #1724, #13885 ) ;
#10852=ORIENTED_EDGE ( 'NONE', *, *, #540, .F. ) ;
#10861=CARTESIAN_POINT ( 'NONE',  ( -40.00000000000000000, 68.00000000000000000, 26.00000000000000355 ) ) ;
#10866=VERTEX_POINT ( 'NONE', #7548 ) ;
#10867=PRESENTATION_STYLE_ASSIGNMENT (( #13365 ) ) ;
#10870=DIRECTION ( 'NONE',  ( -0.000000000000000000, -1.000000000000000000, -0.000000000000000000 ) ) ;
#10906=CARTESIAN_POINT ( 'NONE',  ( -23.00000000000000000, 0.000000000000000000, -31.00000000000005684 ) ) ;
#10935=APPLICATION_CONTEXT ( 'automotive_design' ) ;
#10970=ORIENTED_EDGE ( 'NONE', *, *, #2791, .T. ) ;
#10974=EDGE_CURVE ( 'NONE', #15231, #12156, #10208, .T. ) ;
#10980=PRODUCT_DEFINITION_SHAPE ( 'NONE', 'NONE',  #14195 ) ;
#11003=ORIENTED_EDGE ( 'NONE', *, *, #4887, .T. ) ;
#11012=EDGE_LOOP ( 'NONE', ( #12737, #5528, #12739, #4870 ) ) ;
#11024=ORIENTED_EDGE ( 'NONE', *, *, #10397, .F. ) ;
#11037=VECTOR ( 'NONE', #13114, 1000.000000000000000 ) ;
#11045=VERTEX_POINT ( 'NONE', #3347 ) ;
#11063=VECTOR ( 'NONE', #14784, 1000.000000000000000 ) ;
#11093=VECTOR ( 'NONE', #10497, 1000.000000000000000 ) ;
#11112=ORIENTED_EDGE ( 'NONE', *, *, #5524, .T. ) ;
#11122=DIRECTION ( 'NONE',  ( 0.000000000000000000, 0.000000000000000000, -1.000000000000000000 ) ) ;
#11169=EDGE_LOOP ( 'NONE', ( #3407, #438, #6824, #12369 ) ) ;
#11172=EDGE_LOOP ( 'NONE', ( #457, #467, #5544, #11522, #4960, #1894, #14760, #12479, #5079, #5374, #6365, #11254, #3222, #3693, #3838, #11653 ) ) ;
#11196=EDGE_LOOP ( 'NONE', ( #6158, #6079, #2810, #12471 ) ) ;
#11244=ORIENTED_EDGE ( 'NONE', *, *, #12414, .T. ) ;
#11252=( NAMED_UNIT ( * ) SI_UNIT ( $, .STERADIAN. ) SOLID_ANGLE_UNIT ( ) );
#11254=ORIENTED_EDGE ( 'NONE', *, *, #10522, .F. ) ;
#11263=EDGE_CURVE ( 'NONE', #2294, #15644, #3771, .T. ) ;
#11294=VECTOR ( 'NONE', #16760, 1000.000000000000000 ) ;
#11323=ORIENTED_EDGE ( 'NONE', *, *, #3540, .T. ) ;
#11341=DIRECTION ( 'NONE',  ( 1.000000000000000000, -0.000000000000000000, 0.000000000000000000 ) ) ;
#11348=DIRECTION ( 'NONE',  ( -0.000000000000000000, -1.000000000000000000, 0.000000000000000000 ) ) ;
#11399=EDGE_CURVE ( 'NONE', #14192, #14326, #1353, .T. ) ;
#11410=EDGE_CURVE ( 'NONE', #3442, #16701, #3642, .T. ) ;
#11428=CARTESIAN_POINT ( 'NONE',  ( -25.99999999999999645, 68.00000000000000000, 40.00000000000002132 ) ) ;
#11429=VECTOR ( 'NONE', #11995, 1000.000000000000000 ) ;
#11472=FACE_OUTER_BOUND ( 'NONE', #11196, .T. ) ;
#11497=EDGE_CURVE ( 'NONE', #4223, #4316, #2094, .T. ) ;
#11503=FACE_OUTER_BOUND ( 'NONE', #8012, .T. ) ;
#11507=LINE ( 'NONE', #6333, #9949 ) ;
#11517=EDGE_CURVE ( 'NONE', #11889, #4981, #16605, .T. ) ;
#11518=DIRECTION ( 'NONE',  ( 0.000000000000000000, 0.000000000000000000, -1.000000000000000000 ) ) ;
#11522=ORIENTED_EDGE ( 'NONE', *, *, #5099, .F. ) ;
#11539=DIRECTION ( 'NONE',  ( -0.000000000000000000, -1.000000000000000000, 0.000000000000000000 ) ) ;
#11544=CARTESIAN_POINT ( 'NONE',  ( -25.99999999999999645, 68.00000000000000000, 40.00000000000002132 ) ) ;
#11546=FACE_OUTER_BOUND ( 'NONE', #9958, .T. ) ;
#11565=VECTOR ( 'NONE', #8560, 1000.000000000000000 ) ;
#11569=DIRECTION ( 'NONE',  ( 1.000000000000000000, 0.000000000000000000, 0.000000000000000000 ) ) ;
#11623=VECTOR ( 'NONE', #1302, 1000.000000000000000 ) ;
#11640=VECTOR ( 'NONE', #8745, 1000.000000000000000 ) ;
#11653=ORIENTED_EDGE ( 'NONE', *, *, #12023, .F. ) ;
#11686=EDGE_LOOP ( 'NONE', ( #10970, #1836, #5681, #15012 ) ) ;
#11708=VECTOR ( 'NONE', #7556, 1000.000000000000000 ) ;
#11709=DIRECTION ( 'NONE',  ( -1.000000000000000000, 0.000000000000000000, 0.000000000000000000 ) ) ;
#11711=EDGE_LOOP ( 'NONE', ( #10655, #2845, #11839, #7359 ) ) ;
#11757=CARTESIAN_POINT ( 'NONE',  ( 31.00000000000002842, 68.00000000000000000, 23.00000000000001066 ) ) ;
#11764=DIRECTION ( 'NONE',  ( -0.000000000000000000, -0.000000000000000000, 1.000000000000000000 ) ) ;
#11773=ORIENTED_EDGE ( 'NONE', *, *, #5520, .T. ) ;
#11775=DIRECTION ( 'NONE',  ( -0.000000000000000000, -1.000000000000000000, -0.000000000000000000 ) ) ;
#11782=CARTESIAN_POINT ( 'NONE',  ( -25.99999999999999645, 68.00000000000000000, -39.99999999999999289 ) ) ;
#11793=ADVANCED_BREP_SHAPE_REPRESENTATION ( '', ( #14168, #1488 ), #3145 ) ;
#11794=ORIENTED_EDGE ( 'NONE', *, *, #13617, .F. ) ;
#11796=EDGE_LOOP ( 'NONE', ( #10347, #15643, #1907, #13260 ) ) ;
#11807=DIRECTION ( 'NONE',  ( 0.000000000000000000, 0.000000000000000000, 1.000000000000000000 ) ) ;
#11811=EDGE_CURVE ( 'NONE', #14719, #9593, #16084, .T. ) ;
#11819=ORIENTED_EDGE ( 'NONE', *, *, #15781, .T. ) ;
#11820=ORIENTED_EDGE ( 'NONE', *, *, #9080, .F. ) ;
#11826=CARTESIAN_POINT ( 'NONE',  ( -22.99999999999999645, 68.00000000000000000, 37.00000000000002132 ) ) ;
#11830=DIRECTION ( 'NONE',  ( 0.000000000000000000, 0.000000000000000000, -1.000000000000000000 ) ) ;
#11838=LINE ( 'NONE', #11757, #6609 ) ;
#11839=ORIENTED_EDGE ( 'NONE', *, *, #6660, .T. ) ;
#11840=CIRCLE ( 'NONE', #10201, 4.999999999999997335 ) ;
#11850=CARTESIAN_POINT ( 'NONE',  ( 37.00000000000000000, 68.00000000000000000, 23.00000000000001066 ) ) ;
#11862=DIRECTION ( 'NONE',  ( 0.000000000000000000, 0.000000000000000000, -1.000000000000000000 ) ) ;
#11867=AXIS2_PLACEMENT_3D ( 'NONE', #13634, #823, #4433 ) ;
#11871=ORIENTED_EDGE ( 'NONE', *, *, #8958, .T. ) ;
#11889=VERTEX_POINT ( 'NONE', #1747 ) ;
#11898=CARTESIAN_POINT ( 'NONE',  ( 31.00000000000006395, 68.00000000000000000, -22.99999999999999289 ) ) ;
#11903=AXIS2_PLACEMENT_3D ( 'NONE', #16567, #12537, #857 ) ;
#11926=ORIENTED_EDGE ( 'NONE', *, *, #3121, .F. ) ;
#11930=DIRECTION ( 'NONE',  ( -1.000000000000000000, -0.000000000000000000, -0.000000000000000000 ) ) ;
#11952=CARTESIAN_POINT ( 'NONE',  ( 31.00000000000004263, 0.000000000000000000, -25.99999999999999645 ) ) ;
#11954=AXIS2_PLACEMENT_3D ( 'NONE', #2960, #13273, #4253 ) ;
#11955=CARTESIAN_POINT ( 'NONE',  ( -37.00000000000000000, 68.00000000000000000, 23.00000000000000355 ) ) ;
#11960=VERTEX_POINT ( 'NONE', #13851 ) ;
#11975=CARTESIAN_POINT ( 'NONE',  ( 23.00000000000000711, 68.00000000000000000, -31.00000000000002487 ) ) ;
#11990=ORIENTED_EDGE ( 'NONE', *, *, #16335, .T. ) ;
#11995=DIRECTION ( 'NONE',  ( -1.000000000000000000, -0.000000000000000000, -0.000000000000000000 ) ) ;
#12001=VECTOR ( 'NONE', #215, 1000.000000000000000 ) ;
#12023=EDGE_CURVE ( 'NONE', #8165, #4736, #2077, .T. ) ;
#12049=LINE ( 'NONE', #9562, #4764 ) ;
#12050=ADVANCED_FACE ( 'NONE', ( #7811 ), #13071, .T. ) ;
#12061=EDGE_LOOP ( 'NONE', ( #3240, #5256, #10251, #5070 ) ) ;
#12089=AXIS2_PLACEMENT_3D ( 'NONE', #6208, #10177, #15748 ) ;
#12094=CARTESIAN_POINT ( 'NONE',  ( -22.99999999999999645, 68.00000000000000000, 37.00000000000002132 ) ) ;
#12117=DIRECTION ( 'NONE',  ( -7.709882115452498874E-16, 0.000000000000000000, -1.000000000000000000 ) ) ;
#12152=CARTESIAN_POINT ( 'NONE',  ( -31.00000000000002842, 68.00000000000000000, -25.99999999999999645 ) ) ;
#12156=VERTEX_POINT ( 'NONE', #10400 ) ;
#12163=FACE_OUTER_BOUND ( 'NONE', #3848, .T. ) ;
#12166=CARTESIAN_POINT ( 'NONE',  ( -30.99999999999999645, 68.00000000000000000, -30.99999999999999289 ) ) ;
#12171=CARTESIAN_POINT ( 'NONE',  ( 25.99999999999999645, 0.000000000000000000, 40.00000000000002132 ) ) ;
#12183=DIRECTION ( 'NONE',  ( -0.000000000000000000, -1.000000000000000000, 0.000000000000000000 ) ) ;
#12192=CARTESIAN_POINT ( 'NONE',  ( -25.99999999999999645, 68.00000000000000000, -31.00000000000003197 ) ) ;
#12195=AXIS2_PLACEMENT_3D ( 'NONE', #9803, #2216, #12452 ) ;
#12246=CARTESIAN_POINT ( 'NONE',  ( 40.00000000000000000, 68.00000000000000000, -25.99999999999999645 ) ) ;
#12288=EDGE_LOOP ( 'NONE', ( #7712, #6921, #13773, #13046 ) ) ;
#12293=LINE ( 'NONE', #3104, #1487 ) ;
#12339=ADVANCED_FACE ( 'NONE', ( #15286 ), #7285, .F. ) ;
#12362=AXIS2_PLACEMENT_3D ( 'NONE', #315, #4010, #1516 ) ;
#12369=ORIENTED_EDGE ( 'NONE', *, *, #4830, .T. ) ;
#12377=CARTESIAN_POINT ( 'NONE',  ( -37.00000000000000000, 68.00000000000000000, 23.00000000000000355 ) ) ;
#12414=EDGE_CURVE ( 'NONE', #10866, #10664, #16827, .T. ) ;
#12422=AXIS2_PLACEMENT_3D ( 'NONE', #2721, #12862, #1181 ) ;
#12452=DIRECTION ( 'NONE',  ( 1.156482317317875472E-15, 0.000000000000000000, 1.000000000000000000 ) ) ;
#12462=ORIENTED_EDGE ( 'NONE', *, *, #11410, .F. ) ;
#12463=EDGE_LOOP ( 'NONE', ( #14574, #7226, #13913, #6091 ) ) ;
#12464=AXIS2_PLACEMENT_3D ( 'NONE', #6862, #9464, #6700 ) ;
#12471=ORIENTED_EDGE ( 'NONE', *, *, #387, .T. ) ;
#12476=CARTESIAN_POINT ( 'NONE',  ( -25.99999999999999645, 0.000000000000000000, -39.99999999999999289 ) ) ;
#12478=DIRECTION ( 'NONE',  ( 0.000000000000000000, 0.000000000000000000, -1.000000000000000000 ) ) ;
#12479=ORIENTED_EDGE ( 'NONE', *, *, #2548, .F. ) ;
#12481=DIRECTION ( 'NONE',  ( 1.000000000000000000, 0.000000000000000000, -7.709882115452498874E-16 ) ) ;
#12484=VERTEX_POINT ( 'NONE', #10211 ) ;
#12500=CIRCLE ( 'NONE', #4325, 8.000000000000000000 ) ;
#12501=VECTOR ( 'NONE', #13531, 1000.000000000000000 ) ;
#12514=LINE ( 'NONE', #15263, #11063 ) ;
#12523=VECTOR ( 'NONE', #11930, 1000.000000000000000 ) ;
#12531=ORIENTED_EDGE ( 'NONE', *, *, #15293, .T. ) ;
#12537=DIRECTION ( 'NONE',  ( -0.000000000000000000, -1.000000000000000000, 0.000000000000000000 ) ) ;
#12540=VERTEX_POINT ( 'NONE', #8839 ) ;
#12554=CARTESIAN_POINT ( 'NONE',  ( -31.00000000000002842, 0.000000000000000000, -25.99999999999999645 ) ) ;
#12574=CARTESIAN_POINT ( 'NONE',  ( -25.99999999999999645, 68.00000000000000000, -31.00000000000003197 ) ) ;
#12602=DIRECTION ( 'NONE',  ( -0.000000000000000000, -0.000000000000000000, 1.000000000000000000 ) ) ;
#12645=ADVANCED_FACE ( 'NONE', ( #5652 ), #5299, .F. ) ;
#12649=EDGE_LOOP ( 'NONE', ( #15333, #11926, #8790, #9731 ) ) ;
#12666=ADVANCED_FACE ( 'NONE', ( #7961 ), #6758, .T. ) ;
#12679=VECTOR ( 'NONE', #16791, 1000.000000000000000 ) ;
#12685=DIRECTION ( 'NONE',  ( -1.000000000000000000, -0.000000000000000000, -0.000000000000000000 ) ) ;
#12688=ADVANCED_FACE ( 'NONE', ( #10549 ), #8223, .F. ) ;
#12701=VECTOR ( 'NONE', #1237, 1000.000000000000000 ) ;
#12716=CARTESIAN_POINT ( 'NONE',  ( 30.99999999999999645, 68.00000000000000000, 31.00000000000001066 ) ) ;
#12737=ORIENTED_EDGE ( 'NONE', *, *, #10522, .T. ) ;
#12739=ORIENTED_EDGE ( 'NONE', *, *, #5524, .F. ) ;
#12745=DIRECTION ( 'NONE',  ( -0.000000000000000000, -0.000000000000000000, 1.000000000000000000 ) ) ;
#12749=LINE ( 'NONE', #3645, #2300 ) ;
#12828=CARTESIAN_POINT ( 'NONE',  ( -40.00000000000000000, 68.00000000000000000, 26.00000000000000355 ) ) ;
#12831=CARTESIAN_POINT ( 'NONE',  ( 31.00000000000004263, 68.00000000000000000, -25.99999999999999645 ) ) ;
#12850=DIRECTION ( 'NONE',  ( -1.000000000000000000, 0.000000000000000000, 0.000000000000000000 ) ) ;
#12862=DIRECTION ( 'NONE',  ( -0.000000000000000000, -1.000000000000000000, 0.000000000000000000 ) ) ;
#12877=EDGE_CURVE ( 'NONE', #10758, #5421, #10286, .T. ) ;
#12890=DIRECTION ( 'NONE',  ( -0.000000000000000000, -1.000000000000000000, -0.000000000000000000 ) ) ;
#12910=CARTESIAN_POINT ( 'NONE',  ( 40.00000000000000000, 68.00000000000000000, -25.99999999999999645 ) ) ;
#12928=ADVANCED_FACE ( 'NONE', ( #11472 ), #2286, .T. ) ;
#12961=CYLINDRICAL_SURFACE ( 'NONE', #4515, 5.000000000000000888 ) ;
#12981=LINE ( 'NONE', #7980, #15285 ) ;
#12984=DIRECTION ( 'NONE',  ( 1.000000000000000000, -0.000000000000000000, 0.000000000000000000 ) ) ;
#12990=VECTOR ( 'NONE', #3052, 1000.000000000000000 ) ;
#12996=LINE ( 'NONE', #3806, #11294 ) ;
#13022=LINE ( 'NONE', #1595, #9153 ) ;
#13025=PRODUCT ( 'Servo-Body', 'Servo-Body', '', ( #6088 ) ) ;
#13035=ORIENTED_EDGE ( 'NONE', *, *, #10397, .T. ) ;
#13046=ORIENTED_EDGE ( 'NONE', *, *, #5576, .T. ) ;
#13058=DIRECTION ( 'NONE',  ( -0.000000000000000000, -1.000000000000000000, -0.000000000000000000 ) ) ;
#13071=PLANE ( 'NONE',  #6126 ) ;
#13078=CARTESIAN_POINT ( 'NONE',  ( 31.00000000000002842, 0.000000000000000000, 23.00000000000001066 ) ) ;
#13080=EDGE_CURVE ( 'NONE', #9920, #5349, #16194, .T. ) ;
#13110=PLANE ( 'NONE',  #612 ) ;
#13114=DIRECTION ( 'NONE',  ( -1.000000000000000000, -0.000000000000000000, -0.000000000000000000 ) ) ;
#13143=FACE_OUTER_BOUND ( 'NONE', #11172, .T. ) ;
#13146=ORIENTED_EDGE ( 'NONE', *, *, #10767, .F. ) ;
#13153=ORIENTED_EDGE ( 'NONE', *, *, #14624, .T. ) ;
#13156=CARTESIAN_POINT ( 'NONE',  ( -22.99999999999999645, 68.00000000000000000, 37.00000000000002132 ) ) ;
#13157=ORIENTED_EDGE ( 'NONE', *, *, #14744, .T. ) ;
#13168=AXIS2_PLACEMENT_3D ( 'NONE', #16707, #12850, #7426 ) ;
#13182=DIRECTION ( 'NONE',  ( 0.000000000000000000, 0.000000000000000000, -1.000000000000000000 ) ) ;
#13186=SURFACE_SIDE_STYLE ('',( #6730 ) ) ;
#13214=DIRECTION ( 'NONE',  ( 0.000000000000000000, 0.000000000000000000, 1.000000000000000000 ) ) ;
#13245=AXIS2_PLACEMENT_3D ( 'NONE', #8218, #12183, #11830 ) ;
#13250=CIRCLE ( 'NONE', #12422, 8.000000000000000000 ) ;
#13260=ORIENTED_EDGE ( 'NONE', *, *, #5156, .T. ) ;
#13264=AXIS2_PLACEMENT_3D ( 'NONE', #16950, #11807, #8907 ) ;
#13266=CARTESIAN_POINT ( 'NONE',  ( 25.99999999999999645, 0.000000000000000000, -39.99999999999999289 ) ) ;
#13273=DIRECTION ( 'NONE',  ( 1.000000000000000000, -0.000000000000000000, 0.000000000000000000 ) ) ;
#13283=ORIENTED_EDGE ( 'NONE', *, *, #6982, .T. ) ;
#13324=VECTOR ( 'NONE', #16714, 1000.000000000000000 ) ;
#13325=EDGE_CURVE ( 'NONE', #2083, #6942, #983, .T. ) ;
#13328=DIRECTION ( 'NONE',  ( -0.000000000000000000, -1.000000000000000000, 0.000000000000000000 ) ) ;
#13351=PLANE ( 'NONE',  #8710 ) ;
#13356=DIRECTION ( 'NONE',  ( -0.000000000000000000, -1.000000000000000000, -0.000000000000000000 ) ) ;
#13365=SURFACE_STYLE_USAGE ( .BOTH. , #13186 ) ;
#13393=ORIENTED_EDGE ( 'NONE', *, *, #15374, .T. ) ;
#13434=CARTESIAN_POINT ( 'NONE',  ( -22.99999999999999645, 0.000000000000000000, 37.00000000000002132 ) ) ;
#13448=ORIENTED_EDGE ( 'NONE', *, *, #7179, .F. ) ;
#13456=CARTESIAN_POINT ( 'NONE',  ( -30.99999999999999645, 68.00000000000000000, -30.99999999999999289 ) ) ;
#13459=CARTESIAN_POINT ( 'NONE',  ( -40.00000000000000000, 0.000000000000000000, 26.00000000000000355 ) ) ;
#13466=ORIENTED_EDGE ( 'NONE', *, *, #8561, .T. ) ;
#13476=CARTESIAN_POINT ( 'NONE',  ( -22.99999999999999645, 68.00000000000000000, -36.99999999999999289 ) ) ;
#13485=AXIS2_PLACEMENT_3D ( 'NONE', #1674, #3149, #481 ) ;
#13487=ADVANCED_FACE ( 'NONE', ( #16246 ), #868, .T. ) ;
#13531=DIRECTION ( 'NONE',  ( -0.000000000000000000, -0.000000000000000000, 1.000000000000000000 ) ) ;
#13548=VECTOR ( 'NONE', #13684, 1000.000000000000000 ) ;
#13553=AXIS2_PLACEMENT_3D ( 'NONE', #9212, #12984, #3974 ) ;
#13588=ORIENTED_EDGE ( 'NONE', *, *, #4264, .F. ) ;
#13589=CARTESIAN_POINT ( 'NONE',  ( 23.00000000000000711, 0.000000000000000000, -31.00000000000002487 ) ) ;
#13594=DIRECTION ( 'NONE',  ( -0.000000000000000000, -0.000000000000000000, 1.000000000000000000 ) ) ;
#13613=ORIENTED_EDGE ( 'NONE', *, *, #189, .T. ) ;
#13617=EDGE_CURVE ( 'NONE', #1326, #9930, #15613, .T. ) ;
#13624=FACE_OUTER_BOUND ( 'NONE', #14021, .T. ) ;
#13634=CARTESIAN_POINT ( 'NONE',  ( -25.99999999999999645, 68.00000000000000000, 40.00000000000002132 ) ) ;
#13637=CARTESIAN_POINT ( 'NONE',  ( 30.99999999999999645, 0.000000000000000000, 26.00000000000001066 ) ) ;
#13651=DIRECTION ( 'NONE',  ( -0.000000000000000000, -1.000000000000000000, -0.000000000000000000 ) ) ;
#13673=CARTESIAN_POINT ( 'NONE',  ( 23.00000000000001066, 68.00000000000000000, -36.99999999999999289 ) ) ;
#13681=FACE_OUTER_BOUND ( 'NONE', #7442, .T. ) ;
#13684=DIRECTION ( 'NONE',  ( -0.000000000000000000, -0.000000000000000000, 1.000000000000000000 ) ) ;
#13691=ORIENTED_EDGE ( 'NONE', *, *, #11517, .T. ) ;
#13758=ORIENTED_EDGE ( 'NONE', *, *, #69, .T. ) ;
#13772=VERTEX_POINT ( 'NONE', #3259 ) ;
#13773=ORIENTED_EDGE ( 'NONE', *, *, #7457, .F. ) ;
#13776=CARTESIAN_POINT ( 'NONE',  ( 22.99999999999999289, 68.00000000000000000, 37.00000000000002132 ) ) ;
#13778=CARTESIAN_POINT ( 'NONE',  ( -30.99999999999999645, 68.00000000000000000, -30.99999999999999289 ) ) ;
#13808=CARTESIAN_POINT ( 'NONE',  ( -40.00000000000000000, 68.00000000000000000, -25.99999999999999645 ) ) ;
#13851=CARTESIAN_POINT ( 'NONE',  ( 40.00000000000000000, 68.00000000000000000, 26.00000000000000355 ) ) ;
#13864=CARTESIAN_POINT ( 'NONE',  ( -37.00000000000000000, 0.000000000000000000, 23.00000000000000355 ) ) ;
#13879=LINE ( 'NONE', #7161, #9759 ) ;
#13885=VECTOR ( 'NONE', #1815, 1000.000000000000000 ) ;
#13913=ORIENTED_EDGE ( 'NONE', *, *, #2267, .F. ) ;
#13922=VERTEX_POINT ( 'NONE', #1180 ) ;
#13945=EDGE_LOOP ( 'NONE', ( #11794, #15732, #16345, #13613 ) ) ;
#13947=EDGE_LOOP ( 'NONE', ( #15771, #10411, #10059, #2336 ) ) ;
#13953=CARTESIAN_POINT ( 'NONE',  ( -31.00000000000003197, 68.00000000000000000, -22.99999999999999645 ) ) ;
#13954=CARTESIAN_POINT ( 'NONE',  ( -37.00000000000000000, 68.00000000000000000, 23.00000000000000355 ) ) ;
#14015=CARTESIAN_POINT ( 'NONE',  ( 31.00000000000000711, 68.00000000000000000, -30.99999999999999289 ) ) ;
#14021=EDGE_LOOP ( 'NONE', ( #9462, #3822, #16055, #13283 ) ) ;
#14023=EDGE_CURVE ( 'NONE', #5336, #14967, #8400, .T. ) ;
#14036=CARTESIAN_POINT ( 'NONE',  ( 25.99999999999999645, 68.00000000000000000, 40.00000000000002132 ) ) ;
#14065=DIRECTION ( 'NONE',  ( -0.000000000000000000, -1.000000000000000000, -0.000000000000000000 ) ) ;
#14093=ADVANCED_FACE ( 'NONE', ( #7668 ), #7417, .F. ) ;
#14094=VECTOR ( 'NONE', #9038, 1000.000000000000000 ) ;
#14099=ORIENTED_EDGE ( 'NONE', *, *, #9102, .T. ) ;
#14168=MANIFOLD_SOLID_BREP ( 'Boss-Extrude1', #2502 ) ;
#14192=VERTEX_POINT ( 'NONE', #14819 ) ;
#14195=PRODUCT_DEFINITION ( 'UNKNOWN', '', #16589, #4206 ) ;
#14206=DIRECTION ( 'NONE',  ( -0.000000000000000000, -1.000000000000000000, -0.000000000000000000 ) ) ;
#14214=CARTESIAN_POINT ( 'NONE',  ( -30.99999999999999289, 68.00000000000000000, 31.00000000000000000 ) ) ;
#14254=DIRECTION ( 'NONE',  ( 1.000000000000000000, 0.000000000000000000, 0.000000000000000000 ) ) ;
#14260=ORIENTED_EDGE ( 'NONE', *, *, #16170, .T. ) ;
#14265=DIRECTION ( 'NONE',  ( 1.156482317317883755E-15, -0.000000000000000000, 1.000000000000000000 ) ) ;
#14269=VECTOR ( 'NONE', #3830, 1000.000000000000000 ) ;
#14278=CIRCLE ( 'NONE', #2478, 7.999999999999996447 ) ;
#14291=PLANE ( 'NONE',  #3312 ) ;
#14302=DIRECTION ( 'NONE',  ( -0.000000000000000000, -1.000000000000000000, -0.000000000000000000 ) ) ;
#14308=LINE ( 'NONE', #1085, #12679 ) ;
#14321=ORIENTED_EDGE ( 'NONE', *, *, #4040, .T. ) ;
#14326=VERTEX_POINT ( 'NONE', #5787 ) ;
#14362=VECTOR ( 'NONE', #5531, 1000.000000000000000 ) ;
#14365=ORIENTED_EDGE ( 'NONE', *, *, #11497, .F. ) ;
#14385=FACE_OUTER_BOUND ( 'NONE', #7642, .T. ) ;
#14438=VECTOR ( 'NONE', #946, 1000.000000000000000 ) ;
#14449=LINE ( 'NONE', #13156, #956 ) ;
#14524=ORIENTED_EDGE ( 'NONE', *, *, #8561, .F. ) ;
#14535=DIRECTION ( 'NONE',  ( -0.000000000000000000, -1.000000000000000000, -0.000000000000000000 ) ) ;
#14538=ORIENTED_EDGE ( 'NONE', *, *, #14710, .T. ) ;
#14549=VERTEX_POINT ( 'NONE', #7026 ) ;
#14574=ORIENTED_EDGE ( 'NONE', *, *, #5099, .T. ) ;
#14594=VECTOR ( 'NONE', #14302, 1000.000000000000000 ) ;
#14624=EDGE_CURVE ( 'NONE', #5349, #11960, #5915, .T. ) ;
#14653=CARTESIAN_POINT ( 'NONE',  ( 22.99999999999999289, 68.00000000000000000, 37.00000000000002132 ) ) ;
#14677=ORIENTED_EDGE ( 'NONE', *, *, #8213, .F. ) ;
#14710=EDGE_CURVE ( 'NONE', #6368, #15, #13250, .T. ) ;
#14719=VERTEX_POINT ( 'NONE', #2550 ) ;
#14721=DIRECTION ( 'NONE',  ( -1.000000000000000000, 0.000000000000000000, 0.000000000000000000 ) ) ;
#14744=EDGE_CURVE ( 'NONE', #12540, #15724, #7869, .T. ) ;
#14746=DIRECTION ( 'NONE',  ( 0.000000000000000000, 0.000000000000000000, -1.000000000000000000 ) ) ;
#14760=ORIENTED_EDGE ( 'NONE', *, *, #8927, .F. ) ;
#14775=EDGE_CURVE ( 'NONE', #16153, #3811, #8303, .T. ) ;
#14784=DIRECTION ( 'NONE',  ( -0.000000000000000000, -1.000000000000000000, -0.000000000000000000 ) ) ;
#14797=ORIENTED_EDGE ( 'NONE', *, *, #6702, .T. ) ;
#14815=LINE ( 'NONE', #12152, #5913 ) ;
#14819=CARTESIAN_POINT ( 'NONE',  ( -37.00000000000000000, 68.00000000000000000, -22.99999999999999645 ) ) ;
#14902=LINE ( 'NONE', #12574, #4749 ) ;
#14932=ORIENTED_EDGE ( 'NONE', *, *, #11410, .T. ) ;
#14967=VERTEX_POINT ( 'NONE', #10708 ) ;
#15012=ORIENTED_EDGE ( 'NONE', *, *, #15592, .T. ) ;
#15095=DIRECTION ( 'NONE',  ( 0.000000000000000000, 0.000000000000000000, -1.000000000000000000 ) ) ;
#15113=ORIENTED_EDGE ( 'NONE', *, *, #10974, .T. ) ;
#15141=ADVANCED_FACE ( 'NONE', ( #11546 ), #16784, .F. ) ;
#15146=AXIS2_PLACEMENT_3D ( 'NONE', #2834, #13328, #1886 ) ;
#15157=LINE ( 'NONE', #13078, #11623 ) ;
#15217=DIRECTION ( 'NONE',  ( 1.000000000000000000, 0.000000000000000000, 0.000000000000000000 ) ) ;
#15226=CARTESIAN_POINT ( 'NONE',  ( -37.00000000000000000, 68.00000000000000000, -22.99999999999999645 ) ) ;
#15231=VERTEX_POINT ( 'NONE', #2622 ) ;
#15257=FACE_OUTER_BOUND ( 'NONE', #16264, .T. ) ;
#15263=CARTESIAN_POINT ( 'NONE',  ( 22.99999999999999645, 68.00000000000000000, 31.00000000000006750 ) ) ;
#15269=EDGE_CURVE ( 'NONE', #5852, #15724, #13022, .T. ) ;
#15285=VECTOR ( 'NONE', #12890, 1000.000000000000000 ) ;
#15286=FACE_OUTER_BOUND ( 'NONE', #11796, .T. ) ;
#15291=EDGE_CURVE ( 'NONE', #15586, #13772, #1675, .T. ) ;
#15293=EDGE_CURVE ( 'NONE', #6651, #6319, #2879, .T. ) ;
#15322=CARTESIAN_POINT ( 'NONE',  ( 30.99999999999999645, 68.00000000000000000, 26.00000000000001066 ) ) ;
#15327=PLANE ( 'NONE',  #4199 ) ;
#15333=ORIENTED_EDGE ( 'NONE', *, *, #10334, .F. ) ;
#15353=LINE ( 'NONE', #1264, #4812 ) ;
#15374=EDGE_CURVE ( 'NONE', #7984, #3758, #10692, .T. ) ;
#15417=VECTOR ( 'NONE', #16740, 1000.000000000000000 ) ;
#15437=VECTOR ( 'NONE', #6486, 1000.000000000000000 ) ;
#15448=VERTEX_POINT ( 'NONE', #13864 ) ;
#15450=AXIS2_PLACEMENT_3D ( 'NONE', #6722, #13356, #9233 ) ;
#15508=VERTEX_POINT ( 'NONE', #7323 ) ;
#15524=EDGE_CURVE ( 'NONE', #2162, #10866, #14902, .T. ) ;
#15540=CARTESIAN_POINT ( 'NONE',  ( -22.99999999999999645, 0.000000000000000000, -31.00000000000005684 ) ) ;
#15586=VERTEX_POINT ( 'NONE', #13776 ) ;
#15592=EDGE_CURVE ( 'NONE', #5349, #3811, #16853, .T. ) ;
#15609=EDGE_CURVE ( 'NONE', #14192, #4223, #6195, .T. ) ;
#15613=CIRCLE ( 'NONE', #4645, 8.000000000000000000 ) ;
#15643=ORIENTED_EDGE ( 'NONE', *, *, #16948, .F. ) ;
#15644=VERTEX_POINT ( 'NONE', #3556 ) ;
#15647=VERTEX_POINT ( 'NONE', #8963 ) ;
#15660=ORIENTED_EDGE ( 'NONE', *, *, #4062, .T. ) ;
#15665=CIRCLE ( 'NONE', #9106, 7.999999999999996447 ) ;
#15709=VECTOR ( 'NONE', #2987, 1000.000000000000000 ) ;
#15724=VERTEX_POINT ( 'NONE', #13434 ) ;
#15728=VECTOR ( 'NONE', #12745, 1000.000000000000000 ) ;
#15732=ORIENTED_EDGE ( 'NONE', *, *, #69, .F. ) ;
#15745=CYLINDRICAL_SURFACE ( 'NONE', #2833, 4.999999999999997335 ) ;
#15748=DIRECTION ( 'NONE',  ( 0.000000000000000000, 0.000000000000000000, -1.000000000000000000 ) ) ;
#15753=EDGE_LOOP ( 'NONE', ( #1300, #8343, #12531, #2272 ) ) ;
#15755=EDGE_CURVE ( 'NONE', #14549, #4210, #12049, .T. ) ;
#15758=ORIENTED_EDGE ( 'NONE', *, *, #1417, .T. ) ;
#15759=EDGE_CURVE ( 'NONE', #4224, #10447, #5600, .T. ) ;
#15771=ORIENTED_EDGE ( 'NONE', *, *, #2548, .T. ) ;
#15781=EDGE_CURVE ( 'NONE', #15647, #4736, #5507, .T. ) ;
#15825=ORIENTED_EDGE ( 'NONE', *, *, #9438, .F. ) ;
#15862=APPLICATION_CONTEXT ( 'automotive_design' ) ;
#15872=ORIENTED_EDGE ( 'NONE', *, *, #1439, .F. ) ;
#15881=ORIENTED_EDGE ( 'NONE', *, *, #387, .F. ) ;
#15885=ORIENTED_EDGE ( 'NONE', *, *, #15291, .F. ) ;
#15913=ADVANCED_FACE ( 'NONE', ( #13681 ), #6968, .T. ) ;
#15918=VECTOR ( 'NONE', #2426, 1000.000000000000000 ) ;
#15927=CARTESIAN_POINT ( 'NONE',  ( 31.00000000000006395, 68.00000000000000000, -22.99999999999999289 ) ) ;
#15953=CARTESIAN_POINT ( 'NONE',  ( 22.99999999999999289, 0.000000000000000000, 37.00000000000002132 ) ) ;
#15971=ORIENTED_EDGE ( 'NONE', *, *, #2267, .T. ) ;
#15987=ORIENTED_EDGE ( 'NONE', *, *, #4040, .F. ) ;
#16042=ORIENTED_EDGE ( 'NONE', *, *, #14023, .T. ) ;
#16046=CARTESIAN_POINT ( 'NONE',  ( 31.00000000000004263, 68.00000000000000000, -25.99999999999999645 ) ) ;
#16050=CARTESIAN_POINT ( 'NONE',  ( -23.00000000000000000, 68.00000000000000000, -31.00000000000005684 ) ) ;
#16055=ORIENTED_EDGE ( 'NONE', *, *, #9438, .T. ) ;
#16084=LINE ( 'NONE', #3126, #13548 ) ;
#16092=VECTOR ( 'NONE', #12685, 1000.000000000000000 ) ;
#16102=( NAMED_UNIT ( * ) SI_UNIT ( $, .STERADIAN. ) SOLID_ANGLE_UNIT ( ) );
#16152=PLANE ( 'NONE',  #7840 ) ;
#16153=VERTEX_POINT ( 'NONE', #2579 ) ;
#16170=EDGE_CURVE ( 'NONE', #7984, #2083, #9361, .T. ) ;
#16194=CIRCLE ( 'NONE', #12362, 5.000000000000000888 ) ;
#16237=VECTOR ( 'NONE', #13651, 1000.000000000000000 ) ;
#16246=FACE_OUTER_BOUND ( 'NONE', #9075, .T. ) ;
#16256=VECTOR ( 'NONE', #11569, 1000.000000000000000 ) ;
#16264=EDGE_LOOP ( 'NONE', ( #13588, #16747, #2615, #5474 ) ) ;
#16270=PLANE ( 'NONE',  #13485 ) ;
#16283=PLANE ( 'NONE',  #11867 ) ;
#16290=LINE ( 'NONE', #3065, #16601 ) ;
#16327=CARTESIAN_POINT ( 'NONE',  ( -25.99999999999999645, 0.000000000000000000, 31.00000000000003908 ) ) ;
#16335=EDGE_CURVE ( 'NONE', #3442, #6368, #12514, .T. ) ;
#16345=ORIENTED_EDGE ( 'NONE', *, *, #2341, .T. ) ;
#16349=VECTOR ( 'NONE', #16810, 1000.000000000000000 ) ;
#16373=ORIENTED_EDGE ( 'NONE', *, *, #3050, .T. ) ;
#16375=CARTESIAN_POINT ( 'NONE',  ( -22.99999999999999645, 0.000000000000000000, -36.99999999999999289 ) ) ;
#16394=VECTOR ( 'NONE', #12602, 1000.000000000000000 ) ;
#16405=EDGE_LOOP ( 'NONE', ( #6416, #2084, #2248, #1846 ) ) ;
#16407=CARTESIAN_POINT ( 'NONE',  ( 25.99999999999999645, 0.000000000000000000, 40.00000000000002132 ) ) ;
#16411=ORIENTED_EDGE ( 'NONE', *, *, #15524, .T. ) ;
#16481=DIRECTION ( 'NONE',  ( -0.000000000000000000, -1.000000000000000000, -0.000000000000000000 ) ) ;
#16500=CARTESIAN_POINT ( 'NONE',  ( -31.00000000000002842, 68.00000000000000000, -25.99999999999999645 ) ) ;
#16509=COLOUR_RGB ( '', 0.40784314, 0.44705882, 0.49803922) ;
#16552=VECTOR ( 'NONE', #10253, 1000.000000000000000 ) ;
#16553=CARTESIAN_POINT ( 'NONE',  ( 25.99999999999999645, 68.00000000000000000, 31.00000000000004619 ) ) ;
#16567=CARTESIAN_POINT ( 'NONE',  ( -30.99999999999999645, 0.000000000000000000, -30.99999999999999289 ) ) ;
#16570=LINE ( 'NONE', #9880, #14438 ) ;
#16577=VERTEX_POINT ( 'NONE', #10189 ) ;
#16581=VECTOR ( 'NONE', #96, 1000.000000000000000 ) ;
#16585=DIRECTION ( 'NONE',  ( 0.000000000000000000, 0.000000000000000000, -1.000000000000000000 ) ) ;
#16589=PRODUCT_DEFINITION_FORMATION_WITH_SPECIFIED_SOURCE ( 'ANY', '', #13025, .NOT_KNOWN. ) ;
#16601=VECTOR ( 'NONE', #1785, 1000.000000000000000 ) ;
#16605=LINE ( 'NONE', #12828, #7750 ) ;
#16610=FACE_OUTER_BOUND ( 'NONE', #3596, .T. ) ;
#16619=ADVANCED_FACE ( 'NONE', ( #12163, #400 ), #8202, .F. ) ;
#16678=CARTESIAN_POINT ( 'NONE',  ( -30.99999999999999289, 0.000000000000000000, 31.00000000000000000 ) ) ;
#16685=CARTESIAN_POINT ( 'NONE',  ( -25.99999999999999645, 0.000000000000000000, 40.00000000000002132 ) ) ;
#16701=VERTEX_POINT ( 'NONE', #1514 ) ;
#16707=CARTESIAN_POINT ( 'NONE',  ( 23.00000000000000711, 68.00000000000000000, -31.00000000000002487 ) ) ;
#16714=DIRECTION ( 'NONE',  ( 0.000000000000000000, 0.000000000000000000, -1.000000000000000000 ) ) ;
#16740=DIRECTION ( 'NONE',  ( 5.782411586589399054E-16, 0.000000000000000000, -1.000000000000000000 ) ) ;
#16741=ADVANCED_FACE ( 'NONE', ( #10695 ), #737, .T. ) ;
#16747=ORIENTED_EDGE ( 'NONE', *, *, #3012, .F. ) ;
#16750=CARTESIAN_POINT ( 'NONE',  ( -22.99999999999999645, 68.00000000000000000, -36.99999999999999289 ) ) ;
#16760=DIRECTION ( 'NONE',  ( 0.000000000000000000, 0.000000000000000000, -1.000000000000000000 ) ) ;
#16768=DIRECTION ( 'NONE',  ( 0.000000000000000000, 0.000000000000000000, 1.000000000000000000 ) ) ;
#16784=PLANE ( 'NONE',  #13264 ) ;
#16786=VECTOR ( 'NONE', #7941, 1000.000000000000000 ) ;
#16791=DIRECTION ( 'NONE',  ( -0.000000000000000000, -1.000000000000000000, -0.000000000000000000 ) ) ;
#16808=VECTOR ( 'NONE', #10349, 1000.000000000000000 ) ;
#16810=DIRECTION ( 'NONE',  ( -0.000000000000000000, -0.000000000000000000, 1.000000000000000000 ) ) ;
#16818=DIRECTION ( 'NONE',  ( 0.000000000000000000, 0.000000000000000000, -1.000000000000000000 ) ) ;
#16827=CIRCLE ( 'NONE', #11903, 4.999999999999997335 ) ;
#16841=VECTOR ( 'NONE', #9728, 1000.000000000000000 ) ;
#16850=DIRECTION ( 'NONE',  ( -0.000000000000000000, -1.000000000000000000, -0.000000000000000000 ) ) ;
#16853=LINE ( 'NONE', #15322, #16552 ) ;
#16854=ORIENTED_EDGE ( 'NONE', *, *, #3324, .T. ) ;
#16858=LINE ( 'NONE', #16685, #12701 ) ;
#16883=ORIENTED_EDGE ( 'NONE', *, *, #2341, .F. ) ;
#16885=VECTOR ( 'NONE', #4126, 1000.000000000000000 ) ;
#16921=CARTESIAN_POINT ( 'NONE',  ( -40.00000000000000000, 68.00000000000000000, -25.99999999999999645 ) ) ;
#16947=DIRECTION ( 'NONE',  ( 0.000000000000000000, 0.000000000000000000, -1.000000000000000000 ) ) ;
#16948=EDGE_CURVE ( 'NONE', #5421, #8165, #12749, .T. ) ;
#16950=CARTESIAN_POINT ( 'NONE',  ( -25.99999999999999645, 68.00000000000000000, -39.99999999999999289 ) ) ;
#16952=CARTESIAN_POINT ( 'NONE',  ( -22.99999999999999645, 68.00000000000000000, -31.00000000000005684 ) ) ;
ENDSEC;
END-ISO-10303-21;
